ISO-10303-21;
HEADER;
/* Generated by software containing ST-Developer
 * from STEP Tools, Inc. (www.steptools.com) 
 */

FILE_DESCRIPTION(
/* description */ (''),
/* implementation_level */ '2;1');

FILE_NAME(
/* name */ 'Screw_02.step',
/* time_stamp */ '2026-10-06T13:15:55-07:00',
/* author */ (''),
/* organization */ (''),
/* preprocessor_version */ 'ST-DEVELOPER v20.2',
/* originating_system */ 'Autodesk Translation Framework v15.15.0.0',
/* authorisation */ '');

FILE_SCHEMA (('AUTOMOTIVE_DESIGN { 1 0 10303 214 3 1 1 }'));
ENDSEC;

DATA;
#10=MECHANICAL_DESIGN_GEOMETRIC_PRESENTATION_REPRESENTATION('',(#111),#27707);
#67=ELLIPSE('',#4027,3.36109563026061,2.90329889035631);
#68=ELLIPSE('',#4028,2.84121050972126,2.43735261139454);
#69=ELLIPSE('',#4046,3.33206993022602,2.82346550068506);
#91=SHAPE_REPRESENTATION_RELATIONSHIP('SRR','None',#27748,#101);
#101=ADVANCED_BREP_SHAPE_REPRESENTATION('',(#121),#27700);
#111=STYLED_ITEM('',(#27804),#121);
#121=MANIFOLD_SOLID_BREP('Body1',#3837);
#138=FACE_BOUND('',#765,.T.);
#183=PLANE('',#4009);
#184=PLANE('',#4010);
#185=PLANE('',#4029);
#186=PLANE('',#4050);
#187=PLANE('',#4051);
#236=CIRCLE('',#4012,3.22275);
#237=CIRCLE('',#4026,3.22275);
#238=CIRCLE('',#4030,3.933);
#239=CIRCLE('',#4033,3.933);
#240=CIRCLE('',#4048,5.);
#241=CIRCLE('',#4049,5.);
#353=CYLINDRICAL_SURFACE('',#4011,3.22275);
#354=CYLINDRICAL_SURFACE('',#4013,3.22275);
#355=CYLINDRICAL_SURFACE('',#4014,3.22275);
#356=CYLINDRICAL_SURFACE('',#4015,3.22275);
#357=CYLINDRICAL_SURFACE('',#4016,3.22275);
#358=CYLINDRICAL_SURFACE('',#4017,3.22275);
#359=CYLINDRICAL_SURFACE('',#4018,3.22275);
#360=CYLINDRICAL_SURFACE('',#4019,3.22275);
#361=CYLINDRICAL_SURFACE('',#4020,3.22275);
#362=CYLINDRICAL_SURFACE('',#4021,3.22275);
#363=CYLINDRICAL_SURFACE('',#4022,3.22275);
#364=CYLINDRICAL_SURFACE('',#4023,3.22275);
#365=CYLINDRICAL_SURFACE('',#4024,3.22275);
#366=CYLINDRICAL_SURFACE('',#4025,3.22275);
#367=CYLINDRICAL_SURFACE('',#4031,3.933);
#368=CYLINDRICAL_SURFACE('',#4032,3.933);
#369=CYLINDRICAL_SURFACE('',#4034,3.933);
#370=CYLINDRICAL_SURFACE('',#4035,3.933);
#371=CYLINDRICAL_SURFACE('',#4036,3.933);
#372=CYLINDRICAL_SURFACE('',#4037,3.933);
#373=CYLINDRICAL_SURFACE('',#4038,3.933);
#374=CYLINDRICAL_SURFACE('',#4039,3.933);
#375=CYLINDRICAL_SURFACE('',#4040,3.933);
#376=CYLINDRICAL_SURFACE('',#4041,3.933);
#377=CYLINDRICAL_SURFACE('',#4042,3.933);
#378=CYLINDRICAL_SURFACE('',#4043,3.933);
#379=CYLINDRICAL_SURFACE('',#4044,3.933);
#380=CYLINDRICAL_SURFACE('',#4045,3.933);
#381=CYLINDRICAL_SURFACE('',#4047,5.);
#473=FACE_OUTER_BOUND('',#704,.T.);
#474=FACE_OUTER_BOUND('',#705,.T.);
#475=FACE_OUTER_BOUND('',#706,.T.);
#476=FACE_OUTER_BOUND('',#707,.T.);
#477=FACE_OUTER_BOUND('',#708,.T.);
#478=FACE_OUTER_BOUND('',#709,.T.);
#479=FACE_OUTER_BOUND('',#710,.T.);
#480=FACE_OUTER_BOUND('',#711,.T.);
#481=FACE_OUTER_BOUND('',#712,.T.);
#482=FACE_OUTER_BOUND('',#713,.T.);
#483=FACE_OUTER_BOUND('',#714,.T.);
#484=FACE_OUTER_BOUND('',#715,.T.);
#485=FACE_OUTER_BOUND('',#716,.T.);
#486=FACE_OUTER_BOUND('',#717,.T.);
#487=FACE_OUTER_BOUND('',#718,.T.);
#488=FACE_OUTER_BOUND('',#719,.T.);
#489=FACE_OUTER_BOUND('',#720,.T.);
#490=FACE_OUTER_BOUND('',#721,.T.);
#491=FACE_OUTER_BOUND('',#722,.T.);
#492=FACE_OUTER_BOUND('',#723,.T.);
#493=FACE_OUTER_BOUND('',#724,.T.);
#494=FACE_OUTER_BOUND('',#725,.T.);
#495=FACE_OUTER_BOUND('',#726,.T.);
#496=FACE_OUTER_BOUND('',#727,.T.);
#497=FACE_OUTER_BOUND('',#728,.T.);
#498=FACE_OUTER_BOUND('',#729,.T.);
#499=FACE_OUTER_BOUND('',#730,.T.);
#500=FACE_OUTER_BOUND('',#731,.T.);
#501=FACE_OUTER_BOUND('',#732,.T.);
#502=FACE_OUTER_BOUND('',#733,.T.);
#503=FACE_OUTER_BOUND('',#734,.T.);
#504=FACE_OUTER_BOUND('',#735,.T.);
#505=FACE_OUTER_BOUND('',#736,.T.);
#506=FACE_OUTER_BOUND('',#737,.T.);
#507=FACE_OUTER_BOUND('',#738,.T.);
#508=FACE_OUTER_BOUND('',#739,.T.);
#509=FACE_OUTER_BOUND('',#740,.T.);
#510=FACE_OUTER_BOUND('',#741,.T.);
#511=FACE_OUTER_BOUND('',#742,.T.);
#512=FACE_OUTER_BOUND('',#743,.T.);
#513=FACE_OUTER_BOUND('',#744,.T.);
#514=FACE_OUTER_BOUND('',#745,.T.);
#515=FACE_OUTER_BOUND('',#746,.T.);
#516=FACE_OUTER_BOUND('',#747,.T.);
#517=FACE_OUTER_BOUND('',#748,.T.);
#518=FACE_OUTER_BOUND('',#749,.T.);
#519=FACE_OUTER_BOUND('',#750,.T.);
#520=FACE_OUTER_BOUND('',#751,.T.);
#521=FACE_OUTER_BOUND('',#752,.T.);
#522=FACE_OUTER_BOUND('',#753,.T.);
#523=FACE_OUTER_BOUND('',#754,.T.);
#524=FACE_OUTER_BOUND('',#755,.T.);
#525=FACE_OUTER_BOUND('',#756,.T.);
#526=FACE_OUTER_BOUND('',#757,.T.);
#527=FACE_OUTER_BOUND('',#758,.T.);
#528=FACE_OUTER_BOUND('',#759,.T.);
#529=FACE_OUTER_BOUND('',#760,.T.);
#530=FACE_OUTER_BOUND('',#761,.T.);
#531=FACE_OUTER_BOUND('',#762,.T.);
#532=FACE_OUTER_BOUND('',#763,.T.);
#533=FACE_OUTER_BOUND('',#764,.T.);
#534=FACE_OUTER_BOUND('',#766,.T.);
#704=EDGE_LOOP('',(#2619,#2620,#2621,#2622,#2623,#2624,#2625,#2626,#2627,
#2628,#2629,#2630,#2631,#2632,#2633,#2634,#2635,#2636,#2637,#2638,#2639,
#2640,#2641,#2642,#2643,#2644,#2645,#2646,#2647,#2648,#2649,#2650,#2651,
#2652,#2653,#2654,#2655,#2656,#2657,#2658,#2659,#2660,#2661,#2662,#2663,
#2664,#2665,#2666,#2667,#2668,#2669,#2670,#2671,#2672,#2673));
#705=EDGE_LOOP('',(#2674,#2675,#2676,#2677,#2678,#2679,#2680,#2681,#2682,
#2683,#2684,#2685,#2686,#2687,#2688,#2689,#2690,#2691,#2692,#2693,#2694,
#2695,#2696,#2697,#2698,#2699,#2700,#2701,#2702,#2703,#2704,#2705,#2706,
#2707,#2708,#2709,#2710,#2711,#2712,#2713,#2714,#2715,#2716,#2717,#2718,
#2719,#2720,#2721,#2722,#2723,#2724,#2725,#2726,#2727,#2728));
#706=EDGE_LOOP('',(#2729,#2730,#2731));
#707=EDGE_LOOP('',(#2732,#2733,#2734,#2735));
#708=EDGE_LOOP('',(#2736,#2737,#2738,#2739));
#709=EDGE_LOOP('',(#2740,#2741,#2742,#2743));
#710=EDGE_LOOP('',(#2744,#2745,#2746,#2747));
#711=EDGE_LOOP('',(#2748,#2749,#2750,#2751));
#712=EDGE_LOOP('',(#2752,#2753,#2754,#2755));
#713=EDGE_LOOP('',(#2756,#2757,#2758,#2759));
#714=EDGE_LOOP('',(#2760,#2761,#2762,#2763));
#715=EDGE_LOOP('',(#2764,#2765,#2766,#2767));
#716=EDGE_LOOP('',(#2768,#2769,#2770,#2771));
#717=EDGE_LOOP('',(#2772,#2773,#2774,#2775));
#718=EDGE_LOOP('',(#2776,#2777,#2778,#2779));
#719=EDGE_LOOP('',(#2780,#2781,#2782,#2783));
#720=EDGE_LOOP('',(#2784,#2785,#2786));
#721=EDGE_LOOP('',(#2787,#2788,#2789,#2790,#2791));
#722=EDGE_LOOP('',(#2792,#2793,#2794,#2795));
#723=EDGE_LOOP('',(#2796,#2797,#2798,#2799));
#724=EDGE_LOOP('',(#2800,#2801,#2802,#2803));
#725=EDGE_LOOP('',(#2804,#2805,#2806,#2807));
#726=EDGE_LOOP('',(#2808,#2809,#2810,#2811));
#727=EDGE_LOOP('',(#2812,#2813,#2814,#2815,#2816));
#728=EDGE_LOOP('',(#2817,#2818,#2819,#2820));
#729=EDGE_LOOP('',(#2821,#2822,#2823,#2824));
#730=EDGE_LOOP('',(#2825,#2826,#2827,#2828));
#731=EDGE_LOOP('',(#2829,#2830,#2831,#2832));
#732=EDGE_LOOP('',(#2833,#2834,#2835,#2836));
#733=EDGE_LOOP('',(#2837,#2838,#2839,#2840));
#734=EDGE_LOOP('',(#2841,#2842,#2843,#2844,#2845,#2846));
#735=EDGE_LOOP('',(#2847,#2848,#2849));
#736=EDGE_LOOP('',(#2850,#2851,#2852,#2853));
#737=EDGE_LOOP('',(#2854,#2855,#2856,#2857));
#738=EDGE_LOOP('',(#2858,#2859,#2860,#2861));
#739=EDGE_LOOP('',(#2862,#2863,#2864,#2865));
#740=EDGE_LOOP('',(#2866,#2867,#2868,#2869));
#741=EDGE_LOOP('',(#2870,#2871,#2872,#2873));
#742=EDGE_LOOP('',(#2874,#2875,#2876,#2877));
#743=EDGE_LOOP('',(#2878,#2879,#2880,#2881));
#744=EDGE_LOOP('',(#2882,#2883,#2884,#2885));
#745=EDGE_LOOP('',(#2886,#2887,#2888,#2889));
#746=EDGE_LOOP('',(#2890,#2891,#2892,#2893));
#747=EDGE_LOOP('',(#2894,#2895,#2896,#2897));
#748=EDGE_LOOP('',(#2898,#2899,#2900,#2901));
#749=EDGE_LOOP('',(#2902,#2903,#2904,#2905));
#750=EDGE_LOOP('',(#2906,#2907,#2908,#2909));
#751=EDGE_LOOP('',(#2910,#2911,#2912,#2913));
#752=EDGE_LOOP('',(#2914,#2915,#2916,#2917));
#753=EDGE_LOOP('',(#2918,#2919,#2920,#2921));
#754=EDGE_LOOP('',(#2922,#2923,#2924,#2925));
#755=EDGE_LOOP('',(#2926,#2927,#2928,#2929,#2930));
#756=EDGE_LOOP('',(#2931,#2932,#2933,#2934));
#757=EDGE_LOOP('',(#2935,#2936,#2937,#2938));
#758=EDGE_LOOP('',(#2939,#2940,#2941,#2942));
#759=EDGE_LOOP('',(#2943,#2944,#2945,#2946));
#760=EDGE_LOOP('',(#2947,#2948,#2949,#2950));
#761=EDGE_LOOP('',(#2951,#2952,#2953,#2954,#2955));
#762=EDGE_LOOP('',(#2956,#2957,#2958));
#763=EDGE_LOOP('',(#2959,#2960,#2961,#2962));
#764=EDGE_LOOP('',(#2963));
#765=EDGE_LOOP('',(#2964,#2965,#2966,#2967,#2968,#2969,#2970,#2971));
#766=EDGE_LOOP('',(#2972));
#966=LINE('',#5597,#1142);
#967=LINE('',#5606,#1143);
#968=LINE('',#5617,#1144);
#969=LINE('',#5628,#1145);
#970=LINE('',#5639,#1146);
#971=LINE('',#5650,#1147);
#972=LINE('',#5661,#1148);
#973=LINE('',#5672,#1149);
#974=LINE('',#5683,#1150);
#975=LINE('',#5694,#1151);
#976=LINE('',#5705,#1152);
#977=LINE('',#5716,#1153);
#978=LINE('',#5727,#1154);
#979=LINE('',#5738,#1155);
#980=LINE('',#5740,#1156);
#981=LINE('',#5749,#1157);
#982=LINE('',#5760,#1158);
#983=LINE('',#5771,#1159);
#984=LINE('',#5782,#1160);
#985=LINE('',#5793,#1161);
#986=LINE('',#5804,#1162);
#987=LINE('',#5815,#1163);
#988=LINE('',#5826,#1164);
#989=LINE('',#5837,#1165);
#990=LINE('',#5848,#1166);
#991=LINE('',#5859,#1167);
#992=LINE('',#5870,#1168);
#993=LINE('',#5880,#1169);
#994=LINE('',#5891,#1170);
#995=LINE('',#5902,#1171);
#996=LINE('',#5913,#1172);
#997=LINE('',#5924,#1173);
#998=LINE('',#5935,#1174);
#999=LINE('',#5946,#1175);
#1000=LINE('',#5957,#1176);
#1001=LINE('',#5968,#1177);
#1002=LINE('',#5979,#1178);
#1003=LINE('',#5990,#1179);
#1004=LINE('',#6001,#1180);
#1005=LINE('',#6012,#1181);
#1006=LINE('',#6023,#1182);
#1007=LINE('',#6025,#1183);
#1008=LINE('',#6034,#1184);
#1009=LINE('',#6045,#1185);
#1010=LINE('',#6056,#1186);
#1011=LINE('',#6067,#1187);
#1012=LINE('',#6078,#1188);
#1013=LINE('',#6089,#1189);
#1014=LINE('',#6100,#1190);
#1015=LINE('',#6111,#1191);
#1016=LINE('',#6122,#1192);
#1017=LINE('',#6133,#1193);
#1018=LINE('',#6144,#1194);
#1019=LINE('',#6155,#1195);
#1020=LINE('',#6166,#1196);
#1021=LINE('',#6176,#1197);
#1022=LINE('',#7620,#1198);
#1142=VECTOR('',#4449,10.);
#1143=VECTOR('',#4450,10.);
#1144=VECTOR('',#4451,10.);
#1145=VECTOR('',#4452,10.);
#1146=VECTOR('',#4453,10.);
#1147=VECTOR('',#4454,10.);
#1148=VECTOR('',#4455,10.);
#1149=VECTOR('',#4456,10.);
#1150=VECTOR('',#4457,10.);
#1151=VECTOR('',#4458,10.);
#1152=VECTOR('',#4459,10.);
#1153=VECTOR('',#4460,10.);
#1154=VECTOR('',#4461,10.);
#1155=VECTOR('',#4462,10.);
#1156=VECTOR('',#4463,10.);
#1157=VECTOR('',#4464,10.);
#1158=VECTOR('',#4465,10.);
#1159=VECTOR('',#4466,10.);
#1160=VECTOR('',#4467,10.);
#1161=VECTOR('',#4468,10.);
#1162=VECTOR('',#4469,10.);
#1163=VECTOR('',#4470,10.);
#1164=VECTOR('',#4471,10.);
#1165=VECTOR('',#4472,10.);
#1166=VECTOR('',#4473,10.);
#1167=VECTOR('',#4474,10.);
#1168=VECTOR('',#4475,10.);
#1169=VECTOR('',#4476,10.);
#1170=VECTOR('',#4479,10.);
#1171=VECTOR('',#4480,10.);
#1172=VECTOR('',#4481,10.);
#1173=VECTOR('',#4482,10.);
#1174=VECTOR('',#4483,10.);
#1175=VECTOR('',#4484,10.);
#1176=VECTOR('',#4485,10.);
#1177=VECTOR('',#4486,10.);
#1178=VECTOR('',#4487,10.);
#1179=VECTOR('',#4488,10.);
#1180=VECTOR('',#4489,10.);
#1181=VECTOR('',#4490,10.);
#1182=VECTOR('',#4491,10.);
#1183=VECTOR('',#4492,10.);
#1184=VECTOR('',#4493,10.);
#1185=VECTOR('',#4494,10.);
#1186=VECTOR('',#4495,10.);
#1187=VECTOR('',#4496,10.);
#1188=VECTOR('',#4497,10.);
#1189=VECTOR('',#4498,10.);
#1190=VECTOR('',#4499,10.);
#1191=VECTOR('',#4500,10.);
#1192=VECTOR('',#4501,10.);
#1193=VECTOR('',#4502,10.);
#1194=VECTOR('',#4503,10.);
#1195=VECTOR('',#4504,10.);
#1196=VECTOR('',#4505,10.);
#1197=VECTOR('',#4506,10.);
#1198=VECTOR('',#4583,5.);
#1279=B_SPLINE_CURVE_WITH_KNOTS('',3,(#5588,#5589,#5590,#5591,#5592,#5593,
#5594,#5595),.UNSPECIFIED.,.F.,.F.,(4,2,2,4),(0.,0.000697892015497008,0.0143255677369775,
0.0286350340362092),.UNSPECIFIED.);
#1280=B_SPLINE_CURVE_WITH_KNOTS('',3,(#5599,#5600,#5601,#5602,#5603,#5604),
 .UNSPECIFIED.,.F.,.F.,(4,2,4),(0.,0.0523373446002982,0.104355593610831),
 .UNSPECIFIED.);
#1281=B_SPLINE_CURVE_WITH_KNOTS('',3,(#5608,#5609,#5610,#5611,#5612,#5613,
#5614,#5615),.UNSPECIFIED.,.F.,.F.,(4,2,2,4),(0.,0.00526521584710592,0.0639602373511304,
0.128212067318051),.UNSPECIFIED.);
#1282=B_SPLINE_CURVE_WITH_KNOTS('',3,(#5619,#5620,#5621,#5622,#5623,#5624,
#5625,#5626),.UNSPECIFIED.,.F.,.F.,(4,2,2,4),(0.,0.0627475271162915,0.120075061733582,
0.125236068694296),.UNSPECIFIED.);
#1283=B_SPLINE_CURVE_WITH_KNOTS('',3,(#5630,#5631,#5632,#5633,#5634,#5635,
#5636,#5637),.UNSPECIFIED.,.F.,.F.,(4,2,2,4),(0.,0.00526560282662867,0.0639612078258487,
0.128213120660444),.UNSPECIFIED.);
#1284=B_SPLINE_CURVE_WITH_KNOTS('',3,(#5641,#5642,#5643,#5644,#5645,#5646,
#5647,#5648),.UNSPECIFIED.,.F.,.F.,(4,2,2,4),(0.,0.0627475590562519,0.120075649624267,
0.125237044527633),.UNSPECIFIED.);
#1285=B_SPLINE_CURVE_WITH_KNOTS('',3,(#5652,#5653,#5654,#5655,#5656,#5657,
#5658,#5659),.UNSPECIFIED.,.F.,.F.,(4,2,2,4),(0.,0.00526602648868038,0.0639622680416072,
0.128214273235454),.UNSPECIFIED.);
#1286=B_SPLINE_CURVE_WITH_KNOTS('',3,(#5663,#5664,#5665,#5666,#5667,#5668,
#5669,#5670),.UNSPECIFIED.,.F.,.F.,(4,2,2,4),(0.,0.0627475953399776,0.120076292215752,
0.125238111923284),.UNSPECIFIED.);
#1287=B_SPLINE_CURVE_WITH_KNOTS('',3,(#5674,#5675,#5676,#5677,#5678,#5679,
#5680,#5681),.UNSPECIFIED.,.F.,.F.,(4,2,2,4),(0.,0.00526649276184272,0.0639634322919596,
0.128215541011568),.UNSPECIFIED.);
#1288=B_SPLINE_CURVE_WITH_KNOTS('',3,(#5685,#5686,#5687,#5688,#5689,#5690,
#5691,#5692),.UNSPECIFIED.,.F.,.F.,(4,2,2,4),(0.,0.0627476367935851,0.120076998293466,
0.125239285656593),.UNSPECIFIED.);
#1289=B_SPLINE_CURVE_WITH_KNOTS('',3,(#5696,#5697,#5698,#5699,#5700,#5701,
#5702,#5703),.UNSPECIFIED.,.F.,.F.,(4,2,2,4),(0.,0.00526700898296905,0.0639647182192301,
0.128216943693669),.UNSPECIFIED.);
#1290=B_SPLINE_CURVE_WITH_KNOTS('',3,(#5707,#5708,#5709,#5710,#5711,#5712,
#5713,#5714),.UNSPECIFIED.,.F.,.F.,(4,2,2,4),(0.,0.0627476844547414,0.120077778736361,
0.125240584036134),.UNSPECIFIED.);
#1291=B_SPLINE_CURVE_WITH_KNOTS('',3,(#5718,#5719,#5720,#5721,#5722,#5723,
#5724,#5725),.UNSPECIFIED.,.F.,.F.,(4,2,2,4),(0.,0.0052675843601308,0.0639661480124282,
0.12821850616927),.UNSPECIFIED.);
#1292=B_SPLINE_CURVE_WITH_KNOTS('',3,(#5729,#5730,#5731,#5732,#5733,#5734,
#5735,#5736),.UNSPECIFIED.,.F.,.F.,(4,2,2,4),(0.,0.0627497316200279,0.120007641766305,
0.125309768916132),.UNSPECIFIED.);
#1293=B_SPLINE_CURVE_WITH_KNOTS('',3,(#5742,#5743,#5744,#5745,#5746,#5747),
 .UNSPECIFIED.,.F.,.F.,(4,2,4),(1.75570920373614E-15,0.0320055376006011,
0.0638199285984987),.UNSPECIFIED.);
#1294=B_SPLINE_CURVE_WITH_KNOTS('',3,(#5751,#5752,#5753,#5754,#5755,#5756,
#5757,#5758),.UNSPECIFIED.,.F.,.F.,(4,2,2,4),(0.,0.00526977567755582,0.0639683005470083,
0.128217977351555),.UNSPECIFIED.);
#1295=B_SPLINE_CURVE_WITH_KNOTS('',3,(#5762,#5763,#5764,#5765,#5766,#5767,
#5768,#5769),.UNSPECIFIED.,.F.,.F.,(4,2,2,4),(0.,0.062761494454614,0.120090502459536,
0.125241025317951),.UNSPECIFIED.);
#1296=B_SPLINE_CURVE_WITH_KNOTS('',3,(#5773,#5774,#5775,#5776,#5777,#5778,
#5779,#5780),.UNSPECIFIED.,.F.,.F.,(4,2,2,4),(0.,0.00526922229267531,0.0639669243235216,
0.128216474527037),.UNSPECIFIED.);
#1297=B_SPLINE_CURVE_WITH_KNOTS('',3,(#5784,#5785,#5786,#5787,#5788,#5789,
#5790,#5791),.UNSPECIFIED.,.F.,.F.,(4,2,2,4),(0.,0.0627614441556716,0.120089692527127,
0.125239677665907),.UNSPECIFIED.);
#1298=B_SPLINE_CURVE_WITH_KNOTS('',3,(#5795,#5796,#5797,#5798,#5799,#5800,
#5801,#5802),.UNSPECIFIED.,.F.,.F.,(4,2,2,4),(0.,0.0052687245725873,0.0639656835644766,
0.128215122077758),.UNSPECIFIED.);
#1299=B_SPLINE_CURVE_WITH_KNOTS('',3,(#5806,#5807,#5808,#5809,#5810,#5811,
#5812,#5813),.UNSPECIFIED.,.F.,.F.,(4,2,2,4),(0.,0.0627614005096921,0.120088961436388,
0.125238462177896),.UNSPECIFIED.);
#1300=B_SPLINE_CURVE_WITH_KNOTS('',3,(#5817,#5818,#5819,#5820,#5821,#5822,
#5823,#5824),.UNSPECIFIED.,.F.,.F.,(4,2,2,4),(0.,0.00526827403022492,0.0639645578123657,
0.128213897069805),.UNSPECIFIED.);
#1301=B_SPLINE_CURVE_WITH_KNOTS('',3,(#5828,#5829,#5830,#5831,#5832,#5833,
#5834,#5835),.UNSPECIFIED.,.F.,.F.,(4,2,2,4),(0.,0.0627613623859368,0.12008829741618,
0.125237359044329),.UNSPECIFIED.);
#1302=B_SPLINE_CURVE_WITH_KNOTS('',3,(#5839,#5840,#5841,#5842,#5843,#5844,
#5845,#5846),.UNSPECIFIED.,.F.,.F.,(4,2,2,4),(0.,0.0052678638691292,0.0639635307055346,
0.128212781223319),.UNSPECIFIED.);
#1303=B_SPLINE_CURVE_WITH_KNOTS('',3,(#5850,#5851,#5852,#5853,#5854,#5855,
#5856,#5857),.UNSPECIFIED.,.F.,.F.,(4,2,2,4),(0.,0.0627613288883452,0.120087691004123,
0.125236352349363),.UNSPECIFIED.);
#1304=B_SPLINE_CURVE_WITH_KNOTS('',3,(#5861,#5862,#5863,#5864,#5865,#5866,
#5867,#5868),.UNSPECIFIED.,.F.,.F.,(4,2,2,4),(0.,0.00526748857527077,0.0639625889506368,
0.128211759700356),.UNSPECIFIED.);
#1305=B_SPLINE_CURVE_WITH_KNOTS('',3,(#5872,#5873,#5874,#5875,#5876,#5877,
#5878,#5879),.UNSPECIFIED.,.F.,.F.,(4,2,2,4),(0.,0.0627622351934734,0.120057633553872,
0.125268887079596),.UNSPECIFIED.);
#1306=B_SPLINE_CURVE_WITH_KNOTS('',3,(#5884,#5885,#5886,#5887,#5888,#5889),
 .UNSPECIFIED.,.F.,.F.,(4,2,4),(0.,0.0498589762945784,0.0999595266847454),
 .UNSPECIFIED.);
#1307=B_SPLINE_CURVE_WITH_KNOTS('',3,(#5893,#5894,#5895,#5896,#5897,#5898,
#5899,#5900),.UNSPECIFIED.,.F.,.F.,(4,2,2,4),(0.,0.0627475125621108,0.120074786005034,
0.125235611253279),.UNSPECIFIED.);
#1308=B_SPLINE_CURVE_WITH_KNOTS('',3,(#5904,#5905,#5906,#5907,#5908,#5909,
#5910,#5911),.UNSPECIFIED.,.F.,.F.,(4,2,2,4),(0.,0.00526540507665305,0.0639607121557458,
0.128212582461846),.UNSPECIFIED.);
#1309=B_SPLINE_CURVE_WITH_KNOTS('',3,(#5915,#5916,#5917,#5918,#5919,#5920,
#5921,#5922),.UNSPECIFIED.,.F.,.F.,(4,2,2,4),(0.,0.0627475425879394,0.120075349322764,
0.125236545975591),.UNSPECIFIED.);
#1310=B_SPLINE_CURVE_WITH_KNOTS('',3,(#5926,#5927,#5928,#5929,#5930,#5931,
#5932,#5933),.UNSPECIFIED.,.F.,.F.,(4,2,2,4),(0.,0.00526580973145337,0.0639617259034633,
0.128213683646694),.UNSPECIFIED.);
#1311=B_SPLINE_CURVE_WITH_KNOTS('',3,(#5937,#5938,#5939,#5940,#5941,#5942,
#5943,#5944),.UNSPECIFIED.,.F.,.F.,(4,2,2,4),(0.,0.0627475766076911,0.120075963575788,
0.12523756592846),.UNSPECIFIED.);
#1312=B_SPLINE_CURVE_WITH_KNOTS('',3,(#5948,#5949,#5950,#5951,#5952,#5953,
#5954,#5955),.UNSPECIFIED.,.F.,.F.,(4,2,2,4),(0.,0.00526625387771515,0.063962836142632,
0.128214891577853),.UNSPECIFIED.);
#1313=B_SPLINE_CURVE_WITH_KNOTS('',3,(#5959,#5960,#5961,#5962,#5963,#5964,
#5965,#5966),.UNSPECIFIED.,.F.,.F.,(4,2,2,4),(0.,0.0627476153613634,0.120076636694826,
0.12523868444785),.UNSPECIFIED.);
#1314=B_SPLINE_CURVE_WITH_KNOTS('',3,(#5970,#5971,#5972,#5973,#5974,#5975,
#5976,#5977),.UNSPECIFIED.,.F.,.F.,(4,2,2,4),(0.,0.00526674410433897,0.063964058787172,
0.128216224084347),.UNSPECIFIED.);
#1315=B_SPLINE_CURVE_WITH_KNOTS('',3,(#5981,#5982,#5983,#5984,#5985,#5986,
#5987,#5988),.UNSPECIFIED.,.F.,.F.,(4,2,2,4),(0.,0.0627476597736949,0.120077378440881,
0.125239917954739),.UNSPECIFIED.);
#1316=B_SPLINE_CURVE_WITH_KNOTS('',3,(#5992,#5993,#5994,#5995,#5996,#5997,
#5998,#5999),.UNSPECIFIED.,.F.,.F.,(4,2,2,4),(0.,0.00526728861301724,0.0639654135345664,
0.128217703164965),.UNSPECIFIED.);
#1317=B_SPLINE_CURVE_WITH_KNOTS('',3,(#6003,#6004,#6005,#6006,#6007,#6008,
#6009,#6010),.UNSPECIFIED.,.F.,.F.,(4,2,2,4),(0.,0.0627477110123208,0.120078200979348,
0.125241286926992),.UNSPECIFIED.);
#1318=B_SPLINE_CURVE_WITH_KNOTS('',3,(#6014,#6015,#6016,#6017,#6018,#6019,
#6020,#6021),.UNSPECIFIED.,.F.,.F.,(4,2,2,4),(0.,0.00526789777186566,0.0639669253649914,
0.128219356862823),.UNSPECIFIED.);
#1319=B_SPLINE_CURVE_WITH_KNOTS('',3,(#6027,#6028,#6029,#6030,#6031,#6032),
 .UNSPECIFIED.,.F.,.F.,(4,2,4),(0.,0.0322464693148723,0.0645605482559509),
 .UNSPECIFIED.);
#1320=B_SPLINE_CURVE_WITH_KNOTS('',3,(#6036,#6037,#6038,#6039,#6040,#6041,
#6042,#6043),.UNSPECIFIED.,.F.,.F.,(4,2,2,4),(0.,0.0627615225357567,0.12009094148456,
0.125241756269418),.UNSPECIFIED.);
#1321=B_SPLINE_CURVE_WITH_KNOTS('',3,(#6047,#6048,#6049,#6050,#6051,#6052,
#6053,#6054),.UNSPECIFIED.,.F.,.F.,(4,2,2,4),(0.,0.00526949141755586,0.0639675940491126,
0.128217205528332),.UNSPECIFIED.);
#1322=B_SPLINE_CURVE_WITH_KNOTS('',3,(#6058,#6059,#6060,#6061,#6062,#6063,
#6064,#6065),.UNSPECIFIED.,.F.,.F.,(4,2,2,4),(0.,0.0627614683917021,0.120090086793172,
0.125240333549308),.UNSPECIFIED.);
#1323=B_SPLINE_CURVE_WITH_KNOTS('',3,(#6069,#6070,#6071,#6072,#6073,#6074,
#6075,#6076),.UNSPECIFIED.,.F.,.F.,(4,2,2,4),(0.,0.00526896705103507,0.0639662884118339,
0.128215781088997),.UNSPECIFIED.);
#1324=B_SPLINE_CURVE_WITH_KNOTS('',3,(#6080,#6081,#6082,#6083,#6084,#6085,
#6086,#6087),.UNSPECIFIED.,.F.,.F.,(4,2,2,4),(0.,0.0627614215780341,0.120089317924044,
0.125239054744074),.UNSPECIFIED.);
#1325=B_SPLINE_CURVE_WITH_KNOTS('',3,(#6091,#6092,#6093,#6094,#6095,#6096,
#6097,#6098),.UNSPECIFIED.,.F.,.F.,(4,2,2,4),(0.,0.00526849386310405,0.0639651074163281,
0.128214494876759),.UNSPECIFIED.);
#1326=B_SPLINE_CURVE_WITH_KNOTS('',3,(#6102,#6103,#6104,#6105,#6106,#6107,
#6108,#6109),.UNSPECIFIED.,.F.,.F.,(4,2,2,4),(0.,0.0627613808182858,0.120088621680663,
0.125237897640557),.UNSPECIFIED.);
#1327=B_SPLINE_CURVE_WITH_KNOTS('',3,(#6113,#6114,#6115,#6116,#6117,#6118,
#6119,#6120),.UNSPECIFIED.,.F.,.F.,(4,2,2,4),(0.,0.00526806427303071,0.0639640328250225,
0.128213326505552),.UNSPECIFIED.);
#1328=B_SPLINE_CURVE_WITH_KNOTS('',3,(#6124,#6125,#6126,#6127,#6128,#6129,
#6130,#6131),.UNSPECIFIED.,.F.,.F.,(4,2,2,4),(0.,0.0627613451073725,0.120087987526447,
0.125236844511966),.UNSPECIFIED.);
#1329=B_SPLINE_CURVE_WITH_KNOTS('',3,(#6135,#6136,#6137,#6138,#6139,#6140,
#6141,#6142),.UNSPECIFIED.,.F.,.F.,(4,2,2,4),(0.,0.00526767216729547,0.0639630498969236,
0.128212259500237),.UNSPECIFIED.);
#1330=B_SPLINE_CURVE_WITH_KNOTS('',3,(#6146,#6147,#6148,#6149,#6150,#6151,
#6152,#6153),.UNSPECIFIED.,.F.,.F.,(4,2,2,4),(0.,0.0627613136441549,0.120087406937392,
0.125235881024186),.UNSPECIFIED.);
#1331=B_SPLINE_CURVE_WITH_KNOTS('',3,(#6157,#6158,#6159,#6160,#6161,#6162,
#6163,#6164),.UNSPECIFIED.,.F.,.F.,(4,2,2,4),(0.,0.00526731255574918,0.0639621465613893,
0.128211280360621),.UNSPECIFIED.);
#1332=B_SPLINE_CURVE_WITH_KNOTS('',3,(#6168,#6169,#6170,#6171,#6172,#6173,
#6174,#6175),.UNSPECIFIED.,.F.,.F.,(4,2,2,4),(0.,0.0104628362527636,0.0207308659069718,
0.0209057471409188),.UNSPECIFIED.);
#1333=B_SPLINE_CURVE_WITH_KNOTS('',3,(#6179,#6180,#6181,#6182,#6183,#6184,
#6185,#6186,#6187,#6188,#6189,#6190),.UNSPECIFIED.,.F.,.F.,(4,2,2,2,2,4),
(-0.347751064939877,-0.282575309839093,-0.217361093090031,-0.173962239844469,
-0.0871343728029249,-1.42129173458752E-5),.UNSPECIFIED.);
#1334=B_SPLINE_CURVE_WITH_KNOTS('',3,(#6193,#6194,#6195,#6196,#6197,#6198,
#6199,#6200,#6201,#6202,#6203,#6204,#6205,#6206),.UNSPECIFIED.,.F.,.F.,
(4,2,2,2,2,2,4),(1.00000006515879E-6,0.112920606874871,0.225073242572085,
0.350991141617053,0.476911503870067,0.589070561760002,0.701988545580405),
 .UNSPECIFIED.);
#1335=B_SPLINE_CURVE_WITH_KNOTS('',3,(#6207,#6208,#6209,#6210,#6211,#6212,
#6213,#6214,#6215,#6216,#6217,#6218,#6219,#6220),.UNSPECIFIED.,.F.,.F.,
(4,2,2,2,2,2,4),(-0.701988473605244,-0.589071180819017,-0.4769127850234,
-0.35099108445745,-0.225071862168092,-0.112919904371117,-1.00000006553191E-6),
 .UNSPECIFIED.);
#1336=B_SPLINE_CURVE_WITH_KNOTS('',3,(#6222,#6223,#6224,#6225,#6226,#6227,
#6228,#6229,#6230,#6231,#6232,#6233,#6234,#6235),.UNSPECIFIED.,.F.,.F.,
(4,2,2,2,2,2,4),(-0.701988434327251,-0.589071519766827,-0.476913463798924,
-0.350991050044857,-0.225071122030651,-0.112919515861704,-1.00000006708623E-6),
 .UNSPECIFIED.);
#1337=B_SPLINE_CURVE_WITH_KNOTS('',3,(#6236,#6237,#6238,#6239,#6240,#6241,
#6242,#6243,#6244,#6245,#6246,#6247,#6248,#6249),.UNSPECIFIED.,.F.,.F.,
(4,2,2,2,2,2,4),(1.00000006681659E-6,0.112920186660226,0.225072410288805,
0.350991103825395,0.476912269923873,0.589070928744561,0.701988502664996),
 .UNSPECIFIED.);
#1338=B_SPLINE_CURVE_WITH_KNOTS('',3,(#6251,#6252,#6253,#6254,#6255,#6256,
#6257,#6258,#6259,#6260,#6261,#6262,#6263,#6264),.UNSPECIFIED.,.F.,.F.,
(4,2,2,2,2,2,4),(1.00000006617394E-6,0.112919785545979,0.225071633871698,
0.350991068064418,0.476912983019837,0.589071278822759,0.701988461945112),
 .UNSPECIFIED.);
#1339=B_SPLINE_CURVE_WITH_KNOTS('',3,(#6265,#6266,#6267,#6268,#6269,#6270,
#6271,#6272,#6273,#6274,#6275,#6276,#6277,#6278),.UNSPECIFIED.,.F.,.F.,
(4,2,2,2,2,2,4),(-0.701988396950462,-0.589071843978261,-0.476914097866246,
-0.350991017380745,-0.225070429152157,-0.11291914402688,-1.00000006564294E-6),
 .UNSPECIFIED.);
#1340=B_SPLINE_CURVE_WITH_KNOTS('',3,(#6280,#6281,#6282,#6283,#6284,#6285,
#6286,#6287,#6288,#6289,#6290,#6291,#6292,#6293),.UNSPECIFIED.,.F.,.F.,
(4,2,2,2,2,2,4),(-0.701988361327658,-0.589072154539672,-0.476914691289198,
-0.350990986325078,-0.225069779289555,-0.112918787651099,-1.00000006719725E-6),
 .UNSPECIFIED.);
#1341=B_SPLINE_CURVE_WITH_KNOTS('',3,(#6294,#6295,#6296,#6297,#6298,#6299,
#6300,#6301,#6302,#6303,#6304,#6305,#6306,#6307),.UNSPECIFIED.,.F.,.F.,
(4,2,2,2,2,2,4),(1.00000006582091E-6,0.112919402052754,0.225070908050308,
0.350991034162431,0.476913648211992,0.589071613319107,0.701988423241176),
 .UNSPECIFIED.);
#1342=B_SPLINE_CURVE_WITH_KNOTS('',3,(#6309,#6310,#6311,#6312,#6313,#6314,
#6315,#6316,#6317,#6318,#6319,#6320,#6321,#6322),.UNSPECIFIED.,.F.,.F.,
(4,2,2,2,2,2,4),(1.0000000662017E-6,0.112919034863924,0.225070228189369,
0.350991001967214,0.476914269941965,0.589071933411044,0.701988386393479),
 .UNSPECIFIED.);
#1343=B_SPLINE_CURVE_WITH_KNOTS('',3,(#6323,#6324,#6325,#6326,#6327,#6328,
#6329,#6330,#6331,#6332,#6333,#6334,#6335,#6336),.UNSPECIFIED.,.F.,.F.,
(4,2,2,2,2,2,4),(-0.701988327327066,-0.589072452423603,-0.47691524766257,
-0.350990956752978,-0.225069168686889,-0.112918445645089,-1.00000006486578E-6),
 .UNSPECIFIED.);
#1344=B_SPLINE_CURVE_WITH_KNOTS('',3,(#6338,#6339,#6340,#6341,#6342,#6343,
#6344,#6345,#6346,#6347,#6348,#6349,#6350,#6351),.UNSPECIFIED.,.F.,.F.,
(4,2,2,2,2,2,4),(-0.701988294830502,-0.589072738504006,-0.476915770177297,
-0.350990928552615,-0.225068594007581,-0.112918117029042,-1.00000006530987E-6),
 .UNSPECIFIED.);
#1345=B_SPLINE_CURVE_WITH_KNOTS('',3,(#6352,#6353,#6354,#6355,#6356,#6357,
#6358,#6359,#6360,#6361,#6362,#6363,#6364,#6365),.UNSPECIFIED.,.F.,.F.,
(4,2,2,2,2,2,4),(1.00000006624442E-6,0.112918682802859,0.225069590196386,
0.350990971343344,0.476914852128502,0.589072240149847,0.701988351259665),
 .UNSPECIFIED.);
#1346=B_SPLINE_CURVE_WITH_KNOTS('',3,(#6367,#6368,#6369,#6370,#6371,#6372,
#6373,#6374,#6375,#6376,#6377,#6378,#6379,#6380),.UNSPECIFIED.,.F.,.F.,
(4,2,2,2,2,2,4),(1.00000006535993E-6,0.112918344813946,0.225068990444782,
0.350990942169864,0.476915398241522,0.589072534477526,0.701988317711996),
 .UNSPECIFIED.);
#1347=B_SPLINE_CURVE_WITH_KNOTS('',3,(#6381,#6382,#6383,#6384,#6385,#6386,
#6387,#6388,#6389,#6390,#6391,#6392,#6393,#6394),.UNSPECIFIED.,.F.,.F.,
(4,2,2,2,2,2,4),(-0.70198826373142,-0.589073013568951,-0.476916261675244,
-0.350990901623609,-0.225068052277895,-0.112917800918598,-1.00000006786338E-6),
 .UNSPECIFIED.);
#1348=B_SPLINE_CURVE_WITH_KNOTS('',3,(#6396,#6397,#6398,#6399,#6400,#6401,
#6402,#6403,#6404,#6405,#6406,#6407,#6408,#6409),.UNSPECIFIED.,.F.,.F.,
(4,2,2,2,2,2,4),(-0.701988233933622,-0.589073278331429,-0.476916724695184,
-0.350990875875406,-0.225067540839014,-0.112917496512839,-1.0000000669752E-6),
 .UNSPECIFIED.);
#1349=B_SPLINE_CURVE_WITH_KNOTS('',3,(#6410,#6411,#6412,#6413,#6414,#6415,
#6416,#6417,#6418,#6419,#6420,#6421,#6422,#6423),.UNSPECIFIED.,.F.,.F.,
(4,2,2,2,2,2,4),(1.00000006543456E-6,0.112918019946688,0.225068425709767,
0.35099091433838,0.476915911364266,0.589072817241646,0.701988285635971),
 .UNSPECIFIED.);
#1350=B_SPLINE_CURVE_WITH_KNOTS('',3,(#6425,#6426,#6427,#6428,#6429,#6430,
#6431,#6432,#6433,#6434,#6435,#6436,#6437,#6438),.UNSPECIFIED.,.F.,.F.,
(4,2,2,2,2,2,4),(1.00000006721342E-6,0.112917707342306,0.225067893114481,
0.350990887751436,0.476916394245156,0.589073089207131,0.701988254928176),
 .UNSPECIFIED.);
#1351=B_SPLINE_CURVE_WITH_KNOTS('',3,(#6439,#6440,#6441,#6442,#6443,#6444,
#6445,#6446,#6447,#6448,#6449,#6450,#6451,#6452),.UNSPECIFIED.,.F.,.F.,
(4,2,2,2,2,2,4),(-0.701988205350069,-0.589073533438657,-0.476917161512005,
-0.350990851226291,-0.225067057306856,-0.112917203084259,-1.00000006542089E-6),
 .UNSPECIFIED.);
#1352=B_SPLINE_CURVE_WITH_KNOTS('',3,(#6454,#6455,#6456,#6457,#6458,#6459,
#6460,#6461,#6462,#6463,#6464,#6465,#6466,#6467),.UNSPECIFIED.,.F.,.F.,
(4,2,2,2,2,2,4),(-0.701988177901583,-0.589073779479684,-0.476917574169643,
-0.35099082760215,-0.225066599537539,-0.112916919970041,-1.00000006586498E-6),
 .UNSPECIFIED.);
#1353=B_SPLINE_CURVE_WITH_KNOTS('',3,(#6468,#6469,#6470,#6471,#6472,#6473,
#6474,#6475,#6476,#6477,#6478,#6479,#6480,#6481),.UNSPECIFIED.,.F.,.F.,
(4,2,2,2,2,2,4),(1.0000000653107E-6,0.112917406222399,0.225067390084615,
0.35099086232123,0.476916849341858,0.589073351066865,0.701988225495295),
 .UNSPECIFIED.);
#1354=B_SPLINE_CURVE_WITH_KNOTS('',3,(#6483,#6484,#6485,#6486,#6487,#6488,
#6489,#6490,#6491,#6492,#6493,#6494,#6495,#6496),.UNSPECIFIED.,.F.,.F.,
(4,2,2,2,2,2,4),(1.00000006686074E-6,0.112917115879217,0.22506691430973,
0.35099083796823,0.476917278858146,0.589073603450107,0.701988197252594),
 .UNSPECIFIED.);
#1355=B_SPLINE_CURVE_WITH_KNOTS('',3,(#6497,#6498,#6499,#6500,#6501,#6502,
#6503,#6504,#6505,#6506,#6507,#6508,#6509,#6510),.UNSPECIFIED.,.F.,.F.,
(4,2,2,2,2,2,4),(-0.701988151516124,-0.589074016992278,-0.476917964509549,
-0.350990804935719,-0.225066165598174,-0.11291664656469,-1.00000006575396E-6),
 .UNSPECIFIED.);
#1356=B_SPLINE_CURVE_WITH_KNOTS('',3,(#6512,#6513,#6514,#6515,#6516,#6517,
#6518,#6519,#6520,#6521,#6522,#6523,#6524,#6525),.UNSPECIFIED.,.F.,.F.,
(4,2,2,2,2,2,4),(-0.701988126127907,-0.589074246468584,-0.476918334194806,
-0.350990783165686,-0.225065753741602,-0.112916382313578,-1.000000065976E-6),
 .UNSPECIFIED.);
#1357=B_SPLINE_CURVE_WITH_KNOTS('',3,(#6526,#6527,#6528,#6529,#6530,#6531,
#6532,#6533,#6534,#6535,#6536,#6537,#6538,#6539),.UNSPECIFIED.,.F.,.F.,
(4,2,2,2,2,2,4),(1.00000006463131E-6,0.112916835667461,0.225066463710663,
0.350990814620418,0.476917684775841,0.589073846930262,0.701988170123163),
 .UNSPECIFIED.);
#1358=B_SPLINE_CURVE_WITH_KNOTS('',3,(#6542,#6543,#6544,#6545,#6546,#6547,
#6548,#6549,#6550,#6551,#6552,#6553,#6554,#6555),.UNSPECIFIED.,.F.,.F.,
(4,2,2,2,2,2,4),(3.23003133540915E-5,0.0747831774093426,0.149363713796628,
0.275774683581478,0.338728441304644,0.44478522977372,0.551343968794629),
 .UNSPECIFIED.);
#1359=B_SPLINE_CURVE_WITH_KNOTS('',3,(#6558,#6559,#6560,#6561,#6562,#6563),
 .UNSPECIFIED.,.F.,.F.,(4,2,4),(-0.150154722490422,-0.0750773651805342,
0.),.UNSPECIFIED.);
#1360=B_SPLINE_CURVE_WITH_KNOTS('',3,(#6581,#6582,#6583,#6584),
 .UNSPECIFIED.,.F.,.F.,(4,4),(0.,0.349249092707648),.UNSPECIFIED.);
#1361=B_SPLINE_CURVE_WITH_KNOTS('',3,(#6611,#6612,#6613,#6614,#6615,#6616,
#6617,#6618,#6619,#6620,#6621,#6622,#6623,#6624,#6625,#6626,#6627,#6628,
#6629,#6630,#6631,#6632,#6633,#6634,#6635,#6636,#6637,#6638,#6639,#6640,
#6641,#6642,#6643,#6644,#6645,#6646,#6647,#6648,#6649,#6650,#6651,#6652,
#6653,#6654,#6655,#6656,#6657,#6658,#6659),.UNSPECIFIED.,.F.,.F.,(4,3,3,
3,3,3,3,3,3,3,3,3,3,3,3,3,4),(0.,0.036532739404764,0.0731538029882342,0.109091393921472,
0.133009526612987,0.146488998525985,0.154769879434264,0.190069930149183,
0.204763924687531,0.240416666524628,0.275945870858501,0.295512148258635,
0.303306009056309,0.338041865699653,0.372454604100603,0.40666751045333,
0.414264078313279),.UNSPECIFIED.);
#1362=B_SPLINE_CURVE_WITH_KNOTS('',3,(#6660,#6661,#6662,#6663,#6664),
 .UNSPECIFIED.,.F.,.F.,(4,1,4),(39.5699522859152,40.0185665844411,40.2123850074524),
 .UNSPECIFIED.);
#1363=B_SPLINE_CURVE_WITH_KNOTS('',3,(#6689,#6690,#6691,#6692,#6693,#6694),
 .UNSPECIFIED.,.F.,.F.,(4,1,1,4),(33.2867669787356,33.7353812772616,34.4581548699468,
34.9067691684727),.UNSPECIFIED.);
#1364=B_SPLINE_CURVE_WITH_KNOTS('',3,(#6719,#6720,#6721,#6722,#6723,#6724),
 .UNSPECIFIED.,.F.,.F.,(4,1,1,4),(27.003581671556,27.452195970082,28.1749695627672,
28.6235838612931),.UNSPECIFIED.);
#1365=B_SPLINE_CURVE_WITH_KNOTS('',3,(#6749,#6750,#6751,#6752,#6753,#6754),
 .UNSPECIFIED.,.F.,.F.,(4,1,1,4),(20.7203963643765,21.1690106629024,21.8917842555876,
22.3403985541136),.UNSPECIFIED.);
#1366=B_SPLINE_CURVE_WITH_KNOTS('',3,(#6779,#6780,#6781,#6782,#6783,#6784),
 .UNSPECIFIED.,.F.,.F.,(4,1,1,4),(14.4372110571969,14.8858253557228,15.608598948408,
16.057213246934),.UNSPECIFIED.);
#1367=B_SPLINE_CURVE_WITH_KNOTS('',3,(#6809,#6810,#6811,#6812,#6813,#6814),
 .UNSPECIFIED.,.F.,.F.,(4,1,1,4),(8.15402575001729,8.60264004854321,9.32541364122847,
9.77402793975438),.UNSPECIFIED.);
#1368=B_SPLINE_CURVE_WITH_KNOTS('',3,(#6839,#6840,#6841,#6842,#6843,#6844,
#6845,#6846,#6847,#6848,#6849,#6850,#6851,#6852,#6853,#6854,#6855,#6856,
#6857,#6858,#6859,#6860,#6861,#6862,#6863,#6864,#6865,#6866,#6867,#6868,
#6869,#6870,#6871,#6872,#6873,#6874,#6875,#6876,#6877,#6878,#6879,#6880,
#6881,#6882,#6883,#6884,#6885,#6886,#6887,#6888,#6889,#6890,#6891,#6892,
#6893,#6894,#6895,#6896,#6897,#6898,#6899,#6900,#6901,#6902,#6903,#6904,
#6905),.UNSPECIFIED.,.F.,.F.,(4,3,3,3,3,3,3,3,3,3,3,3,3,3,3,3,3,3,3,3,3,
3,4),(1.87084198259956,1.99926342031853,2.05566622969097,2.13790680565216,
2.14812754057612,2.24061018839636,2.33315480194847,2.36709157385711,2.36709841394138,
2.45784756460922,2.54854382431794,2.63920461494343,2.72984732525151,2.82051706645472,
2.91119807753201,3.00194817584722,3.06604332828347,3.06605017033776,3.1596597536536,
3.2532033890349,3.34670011823176,3.48217495951514,3.49084263257479),
 .UNSPECIFIED.);
#1369=B_SPLINE_CURVE_WITH_KNOTS('',3,(#6931,#6932,#6933,#6934,#6935,#6936),
 .UNSPECIFIED.,.F.,.F.,(4,1,1,4),(36.4283596323254,36.8769739308513,37.5997475235366,
38.0483618220625),.UNSPECIFIED.);
#1370=B_SPLINE_CURVE_WITH_KNOTS('',3,(#6961,#6962,#6963,#6964,#6965,#6966),
 .UNSPECIFIED.,.F.,.F.,(4,1,1,4),(30.1451743251458,30.5937886236718,31.316562216357,
31.7651765148829),.UNSPECIFIED.);
#1371=B_SPLINE_CURVE_WITH_KNOTS('',3,(#6991,#6992,#6993,#6994,#6995,#6996),
 .UNSPECIFIED.,.F.,.F.,(4,1,1,4),(23.8619890179663,24.3106033164922,25.0333769091774,
25.4819912077033),.UNSPECIFIED.);
#1372=B_SPLINE_CURVE_WITH_KNOTS('',3,(#7021,#7022,#7023,#7024,#7025,#7026),
 .UNSPECIFIED.,.F.,.F.,(4,1,1,4),(17.5788037107867,18.0274180093126,18.7501916019978,
19.1988059005238),.UNSPECIFIED.);
#1373=B_SPLINE_CURVE_WITH_KNOTS('',3,(#7051,#7052,#7053,#7054,#7055,#7056),
 .UNSPECIFIED.,.F.,.F.,(4,1,1,4),(11.2956184036071,11.744232702133,12.4670062948183,
12.9156205933442),.UNSPECIFIED.);
#1374=B_SPLINE_CURVE_WITH_KNOTS('',3,(#7081,#7082,#7083,#7084,#7085,#7086),
 .UNSPECIFIED.,.F.,.F.,(4,1,1,4),(5.0124330964275,5.46104739495341,6.18382098763867,
6.63243528616458),.UNSPECIFIED.);
#1375=B_SPLINE_CURVE_WITH_KNOTS('',3,(#7088,#7089,#7090,#7091,#7092,#7093,
#7094,#7095,#7096,#7097,#7098,#7099,#7100,#7101,#7102,#7103,#7104,#7105,
#7106,#7107,#7108,#7109,#7110,#7111,#7112,#7113,#7114,#7115,#7116,#7117,
#7118,#7119,#7120,#7121,#7122,#7123,#7124,#7125,#7126,#7127,#7128,#7129,
#7130),.UNSPECIFIED.,.F.,.F.,(4,3,3,3,3,3,3,3,3,3,3,3,3,3,4),(4.96552804228439E-5,
0.0320183427279736,0.0643403602042524,0.0886933568687708,0.117718239582565,
0.124682181362639,0.131745609822757,0.164253554234894,0.197241305764055,
0.230517869072714,0.25235595445092,0.259992045647903,0.264659623072051,
0.298823823008935,0.320892418579125),.UNSPECIFIED.);
#1376=B_SPLINE_CURVE_WITH_KNOTS('',3,(#7135,#7136,#7137,#7138,#7139,#7140),
 .UNSPECIFIED.,.F.,.F.,(4,1,1,4),(-3.33195380826789,-2.88333950974197,-2.16056591705671,
-2.06120159751576),.UNSPECIFIED.);
#1377=B_SPLINE_CURVE_WITH_KNOTS('',3,(#7143,#7144,#7145,#7146,#7147,#7148,
#7149,#7150,#7151,#7152,#7153,#7154,#7155,#7156,#7157,#7158,#7159,#7160,
#7161,#7162,#7163,#7164,#7165,#7166,#7167,#7168,#7169,#7170,#7171,#7172,
#7173,#7174,#7175,#7176,#7177,#7178,#7179,#7180,#7181,#7182,#7183,#7184,
#7185,#7186,#7187,#7188,#7189,#7190,#7191,#7192,#7193,#7194,#7195,#7196,
#7197,#7198,#7199,#7200,#7201,#7202,#7203),.UNSPECIFIED.,.F.,.F.,(4,3,3,
3,3,3,3,3,3,3,3,3,3,3,3,3,3,3,3,3,4),(-41.0310632895362,-40.9388473190672,
-40.7871353339006,-40.754407737536,-40.6621654402305,-40.5698612720643,
-40.4813329034246,-40.4813266946942,-40.3903969656387,-40.2995162802569,
-40.2086677147606,-40.1178343757824,-40.0269750194882,-39.9361025632024,
-39.8451701195949,-39.8091216443534,-39.8091154310716,-39.7151490717192,
-39.6212411951498,-39.5273766833117,-39.4110634616083),.UNSPECIFIED.);
#1378=B_SPLINE_CURVE_WITH_KNOTS('',3,(#7205,#7206,#7207,#7208,#7209,#7210),
 .UNSPECIFIED.,.F.,.F.,(4,1,1,4),(-37.8894729977556,-37.4408586992297,-36.7180851065444,
-36.2694708080185),.UNSPECIFIED.);
#1379=B_SPLINE_CURVE_WITH_KNOTS('',3,(#7212,#7213,#7214,#7215,#7216,#7217),
 .UNSPECIFIED.,.F.,.F.,(4,1,1,4),(-34.7478803441658,-34.2992660456399,-33.5764924529546,
-33.1278781544287),.UNSPECIFIED.);
#1380=B_SPLINE_CURVE_WITH_KNOTS('',3,(#7219,#7220,#7221,#7222,#7223,#7224),
 .UNSPECIFIED.,.F.,.F.,(4,1,1,4),(-31.606287690576,-31.1576733920501,-30.4348997993648,
-29.9862855008389),.UNSPECIFIED.);
#1381=B_SPLINE_CURVE_WITH_KNOTS('',3,(#7226,#7227,#7228,#7229,#7230,#7231),
 .UNSPECIFIED.,.F.,.F.,(4,1,1,4),(-28.4646950369862,-28.0160807384603,-27.2933071457751,
-26.8446928472491),.UNSPECIFIED.);
#1382=B_SPLINE_CURVE_WITH_KNOTS('',3,(#7233,#7234,#7235,#7236,#7237,#7238),
 .UNSPECIFIED.,.F.,.F.,(4,1,1,4),(-25.3231023833964,-24.8744880848705,-24.1517144921853,
-23.7031001936593),.UNSPECIFIED.);
#1383=B_SPLINE_CURVE_WITH_KNOTS('',3,(#7240,#7241,#7242,#7243,#7244,#7245),
 .UNSPECIFIED.,.F.,.F.,(4,1,1,4),(-22.1815097298066,-21.7328954312807,-21.0101218385955,
-20.5615075400696),.UNSPECIFIED.);
#1384=B_SPLINE_CURVE_WITH_KNOTS('',3,(#7247,#7248,#7249,#7250,#7251,#7252),
 .UNSPECIFIED.,.F.,.F.,(4,1,1,4),(-19.0399170762168,-18.5913027776909,-17.8685291850057,
-17.4199148864798),.UNSPECIFIED.);
#1385=B_SPLINE_CURVE_WITH_KNOTS('',3,(#7254,#7255,#7256,#7257,#7258,#7259),
 .UNSPECIFIED.,.F.,.F.,(4,1,1,4),(-15.8983244226271,-15.4497101241011,-14.7269365314159,
-14.27832223289),.UNSPECIFIED.);
#1386=B_SPLINE_CURVE_WITH_KNOTS('',3,(#7261,#7262,#7263,#7264,#7265,#7266),
 .UNSPECIFIED.,.F.,.F.,(4,1,1,4),(-12.7567317690373,-12.3081174705113,-11.5853438778261,
-11.1367295793002),.UNSPECIFIED.);
#1387=B_SPLINE_CURVE_WITH_KNOTS('',3,(#7268,#7269,#7270,#7271,#7272,#7273),
 .UNSPECIFIED.,.F.,.F.,(4,1,1,4),(-9.61513911544747,-9.16652481692155,-8.4437512242363,
-7.99513692571038),.UNSPECIFIED.);
#1388=B_SPLINE_CURVE_WITH_KNOTS('',3,(#7275,#7276,#7277,#7278,#7279,#7280),
 .UNSPECIFIED.,.F.,.F.,(4,1,1,4),(-6.47354646185768,-6.02493216333176,-5.3021585706465,
-4.85354427212059),.UNSPECIFIED.);
#1389=B_SPLINE_CURVE_WITH_KNOTS('',3,(#7610,#7611,#7612,#7613,#7614,#7615),
 .UNSPECIFIED.,.F.,.F.,(4,2,4),(-0.130044971937413,-0.0647221669300852,
0.),.UNSPECIFIED.);
#1575=VERTEX_POINT('',#5586);
#1576=VERTEX_POINT('',#5587);
#1577=VERTEX_POINT('',#5596);
#1578=VERTEX_POINT('',#5598);
#1579=VERTEX_POINT('',#5605);
#1580=VERTEX_POINT('',#5607);
#1581=VERTEX_POINT('',#5616);
#1582=VERTEX_POINT('',#5618);
#1583=VERTEX_POINT('',#5627);
#1584=VERTEX_POINT('',#5629);
#1585=VERTEX_POINT('',#5638);
#1586=VERTEX_POINT('',#5640);
#1587=VERTEX_POINT('',#5649);
#1588=VERTEX_POINT('',#5651);
#1589=VERTEX_POINT('',#5660);
#1590=VERTEX_POINT('',#5662);
#1591=VERTEX_POINT('',#5671);
#1592=VERTEX_POINT('',#5673);
#1593=VERTEX_POINT('',#5682);
#1594=VERTEX_POINT('',#5684);
#1595=VERTEX_POINT('',#5693);
#1596=VERTEX_POINT('',#5695);
#1597=VERTEX_POINT('',#5704);
#1598=VERTEX_POINT('',#5706);
#1599=VERTEX_POINT('',#5715);
#1600=VERTEX_POINT('',#5717);
#1601=VERTEX_POINT('',#5726);
#1602=VERTEX_POINT('',#5728);
#1603=VERTEX_POINT('',#5737);
#1604=VERTEX_POINT('',#5739);
#1605=VERTEX_POINT('',#5741);
#1606=VERTEX_POINT('',#5748);
#1607=VERTEX_POINT('',#5750);
#1608=VERTEX_POINT('',#5759);
#1609=VERTEX_POINT('',#5761);
#1610=VERTEX_POINT('',#5770);
#1611=VERTEX_POINT('',#5772);
#1612=VERTEX_POINT('',#5781);
#1613=VERTEX_POINT('',#5783);
#1614=VERTEX_POINT('',#5792);
#1615=VERTEX_POINT('',#5794);
#1616=VERTEX_POINT('',#5803);
#1617=VERTEX_POINT('',#5805);
#1618=VERTEX_POINT('',#5814);
#1619=VERTEX_POINT('',#5816);
#1620=VERTEX_POINT('',#5825);
#1621=VERTEX_POINT('',#5827);
#1622=VERTEX_POINT('',#5836);
#1623=VERTEX_POINT('',#5838);
#1624=VERTEX_POINT('',#5847);
#1625=VERTEX_POINT('',#5849);
#1626=VERTEX_POINT('',#5858);
#1627=VERTEX_POINT('',#5860);
#1628=VERTEX_POINT('',#5869);
#1629=VERTEX_POINT('',#5871);
#1630=VERTEX_POINT('',#5882);
#1631=VERTEX_POINT('',#5883);
#1632=VERTEX_POINT('',#5890);
#1633=VERTEX_POINT('',#5892);
#1634=VERTEX_POINT('',#5901);
#1635=VERTEX_POINT('',#5903);
#1636=VERTEX_POINT('',#5912);
#1637=VERTEX_POINT('',#5914);
#1638=VERTEX_POINT('',#5923);
#1639=VERTEX_POINT('',#5925);
#1640=VERTEX_POINT('',#5934);
#1641=VERTEX_POINT('',#5936);
#1642=VERTEX_POINT('',#5945);
#1643=VERTEX_POINT('',#5947);
#1644=VERTEX_POINT('',#5956);
#1645=VERTEX_POINT('',#5958);
#1646=VERTEX_POINT('',#5967);
#1647=VERTEX_POINT('',#5969);
#1648=VERTEX_POINT('',#5978);
#1649=VERTEX_POINT('',#5980);
#1650=VERTEX_POINT('',#5989);
#1651=VERTEX_POINT('',#5991);
#1652=VERTEX_POINT('',#6000);
#1653=VERTEX_POINT('',#6002);
#1654=VERTEX_POINT('',#6011);
#1655=VERTEX_POINT('',#6013);
#1656=VERTEX_POINT('',#6022);
#1657=VERTEX_POINT('',#6024);
#1658=VERTEX_POINT('',#6026);
#1659=VERTEX_POINT('',#6033);
#1660=VERTEX_POINT('',#6035);
#1661=VERTEX_POINT('',#6044);
#1662=VERTEX_POINT('',#6046);
#1663=VERTEX_POINT('',#6055);
#1664=VERTEX_POINT('',#6057);
#1665=VERTEX_POINT('',#6066);
#1666=VERTEX_POINT('',#6068);
#1667=VERTEX_POINT('',#6077);
#1668=VERTEX_POINT('',#6079);
#1669=VERTEX_POINT('',#6088);
#1670=VERTEX_POINT('',#6090);
#1671=VERTEX_POINT('',#6099);
#1672=VERTEX_POINT('',#6101);
#1673=VERTEX_POINT('',#6110);
#1674=VERTEX_POINT('',#6112);
#1675=VERTEX_POINT('',#6121);
#1676=VERTEX_POINT('',#6123);
#1677=VERTEX_POINT('',#6132);
#1678=VERTEX_POINT('',#6134);
#1679=VERTEX_POINT('',#6143);
#1680=VERTEX_POINT('',#6145);
#1681=VERTEX_POINT('',#6154);
#1682=VERTEX_POINT('',#6156);
#1683=VERTEX_POINT('',#6165);
#1684=VERTEX_POINT('',#6167);
#1685=VERTEX_POINT('',#6178);
#1686=VERTEX_POINT('',#6541);
#1687=VERTEX_POINT('',#6556);
#1688=VERTEX_POINT('',#6580);
#1689=VERTEX_POINT('',#6610);
#1690=VERTEX_POINT('',#7134);
#1691=VERTEX_POINT('',#7617);
#1692=VERTEX_POINT('',#7619);
#1979=EDGE_CURVE('',#1575,#1576,#1279,.T.);
#1980=EDGE_CURVE('',#1575,#1577,#966,.T.);
#1981=EDGE_CURVE('',#1578,#1577,#1280,.T.);
#1982=EDGE_CURVE('',#1579,#1578,#967,.T.);
#1983=EDGE_CURVE('',#1580,#1579,#1281,.T.);
#1984=EDGE_CURVE('',#1581,#1580,#968,.T.);
#1985=EDGE_CURVE('',#1582,#1581,#1282,.T.);
#1986=EDGE_CURVE('',#1583,#1582,#969,.T.);
#1987=EDGE_CURVE('',#1584,#1583,#1283,.T.);
#1988=EDGE_CURVE('',#1585,#1584,#970,.T.);
#1989=EDGE_CURVE('',#1586,#1585,#1284,.T.);
#1990=EDGE_CURVE('',#1587,#1586,#971,.T.);
#1991=EDGE_CURVE('',#1588,#1587,#1285,.T.);
#1992=EDGE_CURVE('',#1589,#1588,#972,.T.);
#1993=EDGE_CURVE('',#1590,#1589,#1286,.T.);
#1994=EDGE_CURVE('',#1591,#1590,#973,.T.);
#1995=EDGE_CURVE('',#1592,#1591,#1287,.T.);
#1996=EDGE_CURVE('',#1593,#1592,#974,.T.);
#1997=EDGE_CURVE('',#1594,#1593,#1288,.T.);
#1998=EDGE_CURVE('',#1595,#1594,#975,.T.);
#1999=EDGE_CURVE('',#1596,#1595,#1289,.T.);
#2000=EDGE_CURVE('',#1597,#1596,#976,.T.);
#2001=EDGE_CURVE('',#1598,#1597,#1290,.T.);
#2002=EDGE_CURVE('',#1599,#1598,#977,.T.);
#2003=EDGE_CURVE('',#1600,#1599,#1291,.T.);
#2004=EDGE_CURVE('',#1601,#1600,#978,.T.);
#2005=EDGE_CURVE('',#1602,#1601,#1292,.T.);
#2006=EDGE_CURVE('',#1603,#1602,#979,.T.);
#2007=EDGE_CURVE('',#1604,#1603,#980,.T.);
#2008=EDGE_CURVE('',#1605,#1604,#1293,.T.);
#2009=EDGE_CURVE('',#1606,#1605,#981,.T.);
#2010=EDGE_CURVE('',#1607,#1606,#1294,.T.);
#2011=EDGE_CURVE('',#1608,#1607,#982,.T.);
#2012=EDGE_CURVE('',#1609,#1608,#1295,.T.);
#2013=EDGE_CURVE('',#1610,#1609,#983,.T.);
#2014=EDGE_CURVE('',#1611,#1610,#1296,.T.);
#2015=EDGE_CURVE('',#1612,#1611,#984,.T.);
#2016=EDGE_CURVE('',#1613,#1612,#1297,.T.);
#2017=EDGE_CURVE('',#1614,#1613,#985,.T.);
#2018=EDGE_CURVE('',#1615,#1614,#1298,.T.);
#2019=EDGE_CURVE('',#1616,#1615,#986,.T.);
#2020=EDGE_CURVE('',#1617,#1616,#1299,.T.);
#2021=EDGE_CURVE('',#1618,#1617,#987,.T.);
#2022=EDGE_CURVE('',#1619,#1618,#1300,.T.);
#2023=EDGE_CURVE('',#1620,#1619,#988,.T.);
#2024=EDGE_CURVE('',#1621,#1620,#1301,.T.);
#2025=EDGE_CURVE('',#1622,#1621,#989,.T.);
#2026=EDGE_CURVE('',#1623,#1622,#1302,.T.);
#2027=EDGE_CURVE('',#1624,#1623,#990,.T.);
#2028=EDGE_CURVE('',#1625,#1624,#1303,.T.);
#2029=EDGE_CURVE('',#1626,#1625,#991,.T.);
#2030=EDGE_CURVE('',#1627,#1626,#1304,.T.);
#2031=EDGE_CURVE('',#1628,#1627,#992,.T.);
#2032=EDGE_CURVE('',#1629,#1628,#1305,.T.);
#2033=EDGE_CURVE('',#1576,#1629,#993,.T.);
#2034=EDGE_CURVE('',#1630,#1631,#1306,.T.);
#2035=EDGE_CURVE('',#1632,#1630,#994,.T.);
#2036=EDGE_CURVE('',#1633,#1632,#1307,.T.);
#2037=EDGE_CURVE('',#1634,#1633,#995,.T.);
#2038=EDGE_CURVE('',#1635,#1634,#1308,.T.);
#2039=EDGE_CURVE('',#1636,#1635,#996,.T.);
#2040=EDGE_CURVE('',#1637,#1636,#1309,.T.);
#2041=EDGE_CURVE('',#1638,#1637,#997,.T.);
#2042=EDGE_CURVE('',#1639,#1638,#1310,.T.);
#2043=EDGE_CURVE('',#1640,#1639,#998,.T.);
#2044=EDGE_CURVE('',#1641,#1640,#1311,.T.);
#2045=EDGE_CURVE('',#1642,#1641,#999,.T.);
#2046=EDGE_CURVE('',#1643,#1642,#1312,.T.);
#2047=EDGE_CURVE('',#1644,#1643,#1000,.T.);
#2048=EDGE_CURVE('',#1645,#1644,#1313,.T.);
#2049=EDGE_CURVE('',#1646,#1645,#1001,.T.);
#2050=EDGE_CURVE('',#1647,#1646,#1314,.T.);
#2051=EDGE_CURVE('',#1648,#1647,#1002,.T.);
#2052=EDGE_CURVE('',#1649,#1648,#1315,.T.);
#2053=EDGE_CURVE('',#1650,#1649,#1003,.T.);
#2054=EDGE_CURVE('',#1651,#1650,#1316,.T.);
#2055=EDGE_CURVE('',#1652,#1651,#1004,.T.);
#2056=EDGE_CURVE('',#1653,#1652,#1317,.T.);
#2057=EDGE_CURVE('',#1654,#1653,#1005,.T.);
#2058=EDGE_CURVE('',#1655,#1654,#1318,.T.);
#2059=EDGE_CURVE('',#1656,#1655,#1006,.T.);
#2060=EDGE_CURVE('',#1657,#1656,#1007,.T.);
#2061=EDGE_CURVE('',#1658,#1657,#1319,.T.);
#2062=EDGE_CURVE('',#1659,#1658,#1008,.T.);
#2063=EDGE_CURVE('',#1660,#1659,#1320,.T.);
#2064=EDGE_CURVE('',#1661,#1660,#1009,.T.);
#2065=EDGE_CURVE('',#1662,#1661,#1321,.T.);
#2066=EDGE_CURVE('',#1663,#1662,#1010,.T.);
#2067=EDGE_CURVE('',#1664,#1663,#1322,.T.);
#2068=EDGE_CURVE('',#1665,#1664,#1011,.T.);
#2069=EDGE_CURVE('',#1666,#1665,#1323,.T.);
#2070=EDGE_CURVE('',#1667,#1666,#1012,.T.);
#2071=EDGE_CURVE('',#1668,#1667,#1324,.T.);
#2072=EDGE_CURVE('',#1669,#1668,#1013,.T.);
#2073=EDGE_CURVE('',#1670,#1669,#1325,.T.);
#2074=EDGE_CURVE('',#1671,#1670,#1014,.T.);
#2075=EDGE_CURVE('',#1672,#1671,#1326,.T.);
#2076=EDGE_CURVE('',#1673,#1672,#1015,.T.);
#2077=EDGE_CURVE('',#1674,#1673,#1327,.T.);
#2078=EDGE_CURVE('',#1675,#1674,#1016,.T.);
#2079=EDGE_CURVE('',#1676,#1675,#1328,.T.);
#2080=EDGE_CURVE('',#1677,#1676,#1017,.T.);
#2081=EDGE_CURVE('',#1678,#1677,#1329,.T.);
#2082=EDGE_CURVE('',#1679,#1678,#1018,.T.);
#2083=EDGE_CURVE('',#1680,#1679,#1330,.T.);
#2084=EDGE_CURVE('',#1681,#1680,#1019,.T.);
#2085=EDGE_CURVE('',#1682,#1681,#1331,.T.);
#2086=EDGE_CURVE('',#1683,#1682,#1020,.T.);
#2087=EDGE_CURVE('',#1684,#1683,#1332,.T.);
#2088=EDGE_CURVE('',#1684,#1631,#1021,.T.);
#2089=EDGE_CURVE('',#1602,#1685,#1333,.T.);
#2090=EDGE_CURVE('',#1603,#1685,#236,.T.);
#2091=EDGE_CURVE('',#1654,#1605,#1334,.T.);
#2092=EDGE_CURVE('',#1653,#1606,#1335,.T.);
#2093=EDGE_CURVE('',#1598,#1661,#1336,.T.);
#2094=EDGE_CURVE('',#1599,#1660,#1337,.T.);
#2095=EDGE_CURVE('',#1650,#1609,#1338,.T.);
#2096=EDGE_CURVE('',#1649,#1610,#1339,.T.);
#2097=EDGE_CURVE('',#1594,#1665,#1340,.T.);
#2098=EDGE_CURVE('',#1595,#1664,#1341,.T.);
#2099=EDGE_CURVE('',#1646,#1613,#1342,.T.);
#2100=EDGE_CURVE('',#1645,#1614,#1343,.T.);
#2101=EDGE_CURVE('',#1590,#1669,#1344,.T.);
#2102=EDGE_CURVE('',#1591,#1668,#1345,.T.);
#2103=EDGE_CURVE('',#1642,#1617,#1346,.T.);
#2104=EDGE_CURVE('',#1641,#1618,#1347,.T.);
#2105=EDGE_CURVE('',#1586,#1673,#1348,.T.);
#2106=EDGE_CURVE('',#1587,#1672,#1349,.T.);
#2107=EDGE_CURVE('',#1638,#1621,#1350,.T.);
#2108=EDGE_CURVE('',#1637,#1622,#1351,.T.);
#2109=EDGE_CURVE('',#1582,#1677,#1352,.T.);
#2110=EDGE_CURVE('',#1583,#1676,#1353,.T.);
#2111=EDGE_CURVE('',#1634,#1625,#1354,.T.);
#2112=EDGE_CURVE('',#1633,#1626,#1355,.T.);
#2113=EDGE_CURVE('',#1578,#1681,#1356,.T.);
#2114=EDGE_CURVE('',#1579,#1680,#1357,.T.);
#2115=EDGE_CURVE('',#1686,#1629,#1358,.T.);
#2116=EDGE_CURVE('',#1687,#1686,#237,.T.);
#2117=EDGE_CURVE('',#1687,#1576,#1359,.T.);
#2118=EDGE_CURVE('',#1688,#1683,#1360,.T.);
#2119=EDGE_CURVE('',#1684,#1688,#67,.T.);
#2120=EDGE_CURVE('',#1689,#1604,#1361,.T.);
#2121=EDGE_CURVE('',#1655,#1689,#1362,.T.);
#2122=EDGE_CURVE('',#1651,#1608,#1363,.T.);
#2123=EDGE_CURVE('',#1647,#1612,#1364,.T.);
#2124=EDGE_CURVE('',#1643,#1616,#1365,.T.);
#2125=EDGE_CURVE('',#1639,#1620,#1366,.T.);
#2126=EDGE_CURVE('',#1635,#1624,#1367,.T.);
#2127=EDGE_CURVE('',#1630,#1628,#1368,.T.);
#2128=EDGE_CURVE('',#1686,#1631,#68,.T.);
#2129=EDGE_CURVE('',#1600,#1659,#1369,.T.);
#2130=EDGE_CURVE('',#1596,#1663,#1370,.T.);
#2131=EDGE_CURVE('',#1592,#1667,#1371,.T.);
#2132=EDGE_CURVE('',#1588,#1671,#1372,.T.);
#2133=EDGE_CURVE('',#1584,#1675,#1373,.T.);
#2134=EDGE_CURVE('',#1580,#1679,#1374,.T.);
#2135=EDGE_CURVE('',#1685,#1657,#1375,.T.);
#2136=EDGE_CURVE('',#1656,#1689,#238,.F.);
#2137=EDGE_CURVE('',#1682,#1690,#1376,.T.);
#2138=EDGE_CURVE('',#1688,#1690,#239,.T.);
#2139=EDGE_CURVE('',#1658,#1601,#1377,.T.);
#2140=EDGE_CURVE('',#1607,#1652,#1378,.T.);
#2141=EDGE_CURVE('',#1662,#1597,#1379,.T.);
#2142=EDGE_CURVE('',#1611,#1648,#1380,.T.);
#2143=EDGE_CURVE('',#1666,#1593,#1381,.T.);
#2144=EDGE_CURVE('',#1615,#1644,#1382,.T.);
#2145=EDGE_CURVE('',#1670,#1589,#1383,.T.);
#2146=EDGE_CURVE('',#1619,#1640,#1384,.T.);
#2147=EDGE_CURVE('',#1674,#1585,#1385,.T.);
#2148=EDGE_CURVE('',#1623,#1636,#1386,.T.);
#2149=EDGE_CURVE('',#1678,#1581,#1387,.T.);
#2150=EDGE_CURVE('',#1627,#1632,#1388,.T.);
#2151=EDGE_CURVE('',#1690,#1577,#69,.T.);
#2152=EDGE_CURVE('',#1575,#1687,#1389,.T.);
#2153=EDGE_CURVE('',#1691,#1691,#240,.T.);
#2154=EDGE_CURVE('',#1691,#1692,#1022,.T.);
#2155=EDGE_CURVE('',#1692,#1692,#241,.T.);
#2619=ORIENTED_EDGE('',*,*,#1979,.F.);
#2620=ORIENTED_EDGE('',*,*,#1980,.T.);
#2621=ORIENTED_EDGE('',*,*,#1981,.F.);
#2622=ORIENTED_EDGE('',*,*,#1982,.F.);
#2623=ORIENTED_EDGE('',*,*,#1983,.F.);
#2624=ORIENTED_EDGE('',*,*,#1984,.F.);
#2625=ORIENTED_EDGE('',*,*,#1985,.F.);
#2626=ORIENTED_EDGE('',*,*,#1986,.F.);
#2627=ORIENTED_EDGE('',*,*,#1987,.F.);
#2628=ORIENTED_EDGE('',*,*,#1988,.F.);
#2629=ORIENTED_EDGE('',*,*,#1989,.F.);
#2630=ORIENTED_EDGE('',*,*,#1990,.F.);
#2631=ORIENTED_EDGE('',*,*,#1991,.F.);
#2632=ORIENTED_EDGE('',*,*,#1992,.F.);
#2633=ORIENTED_EDGE('',*,*,#1993,.F.);
#2634=ORIENTED_EDGE('',*,*,#1994,.F.);
#2635=ORIENTED_EDGE('',*,*,#1995,.F.);
#2636=ORIENTED_EDGE('',*,*,#1996,.F.);
#2637=ORIENTED_EDGE('',*,*,#1997,.F.);
#2638=ORIENTED_EDGE('',*,*,#1998,.F.);
#2639=ORIENTED_EDGE('',*,*,#1999,.F.);
#2640=ORIENTED_EDGE('',*,*,#2000,.F.);
#2641=ORIENTED_EDGE('',*,*,#2001,.F.);
#2642=ORIENTED_EDGE('',*,*,#2002,.F.);
#2643=ORIENTED_EDGE('',*,*,#2003,.F.);
#2644=ORIENTED_EDGE('',*,*,#2004,.F.);
#2645=ORIENTED_EDGE('',*,*,#2005,.F.);
#2646=ORIENTED_EDGE('',*,*,#2006,.F.);
#2647=ORIENTED_EDGE('',*,*,#2007,.F.);
#2648=ORIENTED_EDGE('',*,*,#2008,.F.);
#2649=ORIENTED_EDGE('',*,*,#2009,.F.);
#2650=ORIENTED_EDGE('',*,*,#2010,.F.);
#2651=ORIENTED_EDGE('',*,*,#2011,.F.);
#2652=ORIENTED_EDGE('',*,*,#2012,.F.);
#2653=ORIENTED_EDGE('',*,*,#2013,.F.);
#2654=ORIENTED_EDGE('',*,*,#2014,.F.);
#2655=ORIENTED_EDGE('',*,*,#2015,.F.);
#2656=ORIENTED_EDGE('',*,*,#2016,.F.);
#2657=ORIENTED_EDGE('',*,*,#2017,.F.);
#2658=ORIENTED_EDGE('',*,*,#2018,.F.);
#2659=ORIENTED_EDGE('',*,*,#2019,.F.);
#2660=ORIENTED_EDGE('',*,*,#2020,.F.);
#2661=ORIENTED_EDGE('',*,*,#2021,.F.);
#2662=ORIENTED_EDGE('',*,*,#2022,.F.);
#2663=ORIENTED_EDGE('',*,*,#2023,.F.);
#2664=ORIENTED_EDGE('',*,*,#2024,.F.);
#2665=ORIENTED_EDGE('',*,*,#2025,.F.);
#2666=ORIENTED_EDGE('',*,*,#2026,.F.);
#2667=ORIENTED_EDGE('',*,*,#2027,.F.);
#2668=ORIENTED_EDGE('',*,*,#2028,.F.);
#2669=ORIENTED_EDGE('',*,*,#2029,.F.);
#2670=ORIENTED_EDGE('',*,*,#2030,.F.);
#2671=ORIENTED_EDGE('',*,*,#2031,.F.);
#2672=ORIENTED_EDGE('',*,*,#2032,.F.);
#2673=ORIENTED_EDGE('',*,*,#2033,.F.);
#2674=ORIENTED_EDGE('',*,*,#2034,.F.);
#2675=ORIENTED_EDGE('',*,*,#2035,.F.);
#2676=ORIENTED_EDGE('',*,*,#2036,.F.);
#2677=ORIENTED_EDGE('',*,*,#2037,.F.);
#2678=ORIENTED_EDGE('',*,*,#2038,.F.);
#2679=ORIENTED_EDGE('',*,*,#2039,.F.);
#2680=ORIENTED_EDGE('',*,*,#2040,.F.);
#2681=ORIENTED_EDGE('',*,*,#2041,.F.);
#2682=ORIENTED_EDGE('',*,*,#2042,.F.);
#2683=ORIENTED_EDGE('',*,*,#2043,.F.);
#2684=ORIENTED_EDGE('',*,*,#2044,.F.);
#2685=ORIENTED_EDGE('',*,*,#2045,.F.);
#2686=ORIENTED_EDGE('',*,*,#2046,.F.);
#2687=ORIENTED_EDGE('',*,*,#2047,.F.);
#2688=ORIENTED_EDGE('',*,*,#2048,.F.);
#2689=ORIENTED_EDGE('',*,*,#2049,.F.);
#2690=ORIENTED_EDGE('',*,*,#2050,.F.);
#2691=ORIENTED_EDGE('',*,*,#2051,.F.);
#2692=ORIENTED_EDGE('',*,*,#2052,.F.);
#2693=ORIENTED_EDGE('',*,*,#2053,.F.);
#2694=ORIENTED_EDGE('',*,*,#2054,.F.);
#2695=ORIENTED_EDGE('',*,*,#2055,.F.);
#2696=ORIENTED_EDGE('',*,*,#2056,.F.);
#2697=ORIENTED_EDGE('',*,*,#2057,.F.);
#2698=ORIENTED_EDGE('',*,*,#2058,.F.);
#2699=ORIENTED_EDGE('',*,*,#2059,.F.);
#2700=ORIENTED_EDGE('',*,*,#2060,.F.);
#2701=ORIENTED_EDGE('',*,*,#2061,.F.);
#2702=ORIENTED_EDGE('',*,*,#2062,.F.);
#2703=ORIENTED_EDGE('',*,*,#2063,.F.);
#2704=ORIENTED_EDGE('',*,*,#2064,.F.);
#2705=ORIENTED_EDGE('',*,*,#2065,.F.);
#2706=ORIENTED_EDGE('',*,*,#2066,.F.);
#2707=ORIENTED_EDGE('',*,*,#2067,.F.);
#2708=ORIENTED_EDGE('',*,*,#2068,.F.);
#2709=ORIENTED_EDGE('',*,*,#2069,.F.);
#2710=ORIENTED_EDGE('',*,*,#2070,.F.);
#2711=ORIENTED_EDGE('',*,*,#2071,.F.);
#2712=ORIENTED_EDGE('',*,*,#2072,.F.);
#2713=ORIENTED_EDGE('',*,*,#2073,.F.);
#2714=ORIENTED_EDGE('',*,*,#2074,.F.);
#2715=ORIENTED_EDGE('',*,*,#2075,.F.);
#2716=ORIENTED_EDGE('',*,*,#2076,.F.);
#2717=ORIENTED_EDGE('',*,*,#2077,.F.);
#2718=ORIENTED_EDGE('',*,*,#2078,.F.);
#2719=ORIENTED_EDGE('',*,*,#2079,.F.);
#2720=ORIENTED_EDGE('',*,*,#2080,.F.);
#2721=ORIENTED_EDGE('',*,*,#2081,.F.);
#2722=ORIENTED_EDGE('',*,*,#2082,.F.);
#2723=ORIENTED_EDGE('',*,*,#2083,.F.);
#2724=ORIENTED_EDGE('',*,*,#2084,.F.);
#2725=ORIENTED_EDGE('',*,*,#2085,.F.);
#2726=ORIENTED_EDGE('',*,*,#2086,.F.);
#2727=ORIENTED_EDGE('',*,*,#2087,.F.);
#2728=ORIENTED_EDGE('',*,*,#2088,.T.);
#2729=ORIENTED_EDGE('',*,*,#2006,.T.);
#2730=ORIENTED_EDGE('',*,*,#2089,.T.);
#2731=ORIENTED_EDGE('',*,*,#2090,.F.);
#2732=ORIENTED_EDGE('',*,*,#2009,.T.);
#2733=ORIENTED_EDGE('',*,*,#2091,.F.);
#2734=ORIENTED_EDGE('',*,*,#2057,.T.);
#2735=ORIENTED_EDGE('',*,*,#2092,.T.);
#2736=ORIENTED_EDGE('',*,*,#2002,.T.);
#2737=ORIENTED_EDGE('',*,*,#2093,.T.);
#2738=ORIENTED_EDGE('',*,*,#2064,.T.);
#2739=ORIENTED_EDGE('',*,*,#2094,.F.);
#2740=ORIENTED_EDGE('',*,*,#2013,.T.);
#2741=ORIENTED_EDGE('',*,*,#2095,.F.);
#2742=ORIENTED_EDGE('',*,*,#2053,.T.);
#2743=ORIENTED_EDGE('',*,*,#2096,.T.);
#2744=ORIENTED_EDGE('',*,*,#1998,.T.);
#2745=ORIENTED_EDGE('',*,*,#2097,.T.);
#2746=ORIENTED_EDGE('',*,*,#2068,.T.);
#2747=ORIENTED_EDGE('',*,*,#2098,.F.);
#2748=ORIENTED_EDGE('',*,*,#2017,.T.);
#2749=ORIENTED_EDGE('',*,*,#2099,.F.);
#2750=ORIENTED_EDGE('',*,*,#2049,.T.);
#2751=ORIENTED_EDGE('',*,*,#2100,.T.);
#2752=ORIENTED_EDGE('',*,*,#1994,.T.);
#2753=ORIENTED_EDGE('',*,*,#2101,.T.);
#2754=ORIENTED_EDGE('',*,*,#2072,.T.);
#2755=ORIENTED_EDGE('',*,*,#2102,.F.);
#2756=ORIENTED_EDGE('',*,*,#2021,.T.);
#2757=ORIENTED_EDGE('',*,*,#2103,.F.);
#2758=ORIENTED_EDGE('',*,*,#2045,.T.);
#2759=ORIENTED_EDGE('',*,*,#2104,.T.);
#2760=ORIENTED_EDGE('',*,*,#1990,.T.);
#2761=ORIENTED_EDGE('',*,*,#2105,.T.);
#2762=ORIENTED_EDGE('',*,*,#2076,.T.);
#2763=ORIENTED_EDGE('',*,*,#2106,.F.);
#2764=ORIENTED_EDGE('',*,*,#2025,.T.);
#2765=ORIENTED_EDGE('',*,*,#2107,.F.);
#2766=ORIENTED_EDGE('',*,*,#2041,.T.);
#2767=ORIENTED_EDGE('',*,*,#2108,.T.);
#2768=ORIENTED_EDGE('',*,*,#1986,.T.);
#2769=ORIENTED_EDGE('',*,*,#2109,.T.);
#2770=ORIENTED_EDGE('',*,*,#2080,.T.);
#2771=ORIENTED_EDGE('',*,*,#2110,.F.);
#2772=ORIENTED_EDGE('',*,*,#2029,.T.);
#2773=ORIENTED_EDGE('',*,*,#2111,.F.);
#2774=ORIENTED_EDGE('',*,*,#2037,.T.);
#2775=ORIENTED_EDGE('',*,*,#2112,.T.);
#2776=ORIENTED_EDGE('',*,*,#1982,.T.);
#2777=ORIENTED_EDGE('',*,*,#2113,.T.);
#2778=ORIENTED_EDGE('',*,*,#2084,.T.);
#2779=ORIENTED_EDGE('',*,*,#2114,.F.);
#2780=ORIENTED_EDGE('',*,*,#2033,.T.);
#2781=ORIENTED_EDGE('',*,*,#2115,.F.);
#2782=ORIENTED_EDGE('',*,*,#2116,.F.);
#2783=ORIENTED_EDGE('',*,*,#2117,.T.);
#2784=ORIENTED_EDGE('',*,*,#2087,.T.);
#2785=ORIENTED_EDGE('',*,*,#2118,.F.);
#2786=ORIENTED_EDGE('',*,*,#2119,.F.);
#2787=ORIENTED_EDGE('',*,*,#2008,.T.);
#2788=ORIENTED_EDGE('',*,*,#2120,.F.);
#2789=ORIENTED_EDGE('',*,*,#2121,.F.);
#2790=ORIENTED_EDGE('',*,*,#2058,.T.);
#2791=ORIENTED_EDGE('',*,*,#2091,.T.);
#2792=ORIENTED_EDGE('',*,*,#2012,.T.);
#2793=ORIENTED_EDGE('',*,*,#2122,.F.);
#2794=ORIENTED_EDGE('',*,*,#2054,.T.);
#2795=ORIENTED_EDGE('',*,*,#2095,.T.);
#2796=ORIENTED_EDGE('',*,*,#2016,.T.);
#2797=ORIENTED_EDGE('',*,*,#2123,.F.);
#2798=ORIENTED_EDGE('',*,*,#2050,.T.);
#2799=ORIENTED_EDGE('',*,*,#2099,.T.);
#2800=ORIENTED_EDGE('',*,*,#2020,.T.);
#2801=ORIENTED_EDGE('',*,*,#2124,.F.);
#2802=ORIENTED_EDGE('',*,*,#2046,.T.);
#2803=ORIENTED_EDGE('',*,*,#2103,.T.);
#2804=ORIENTED_EDGE('',*,*,#2024,.T.);
#2805=ORIENTED_EDGE('',*,*,#2125,.F.);
#2806=ORIENTED_EDGE('',*,*,#2042,.T.);
#2807=ORIENTED_EDGE('',*,*,#2107,.T.);
#2808=ORIENTED_EDGE('',*,*,#2028,.T.);
#2809=ORIENTED_EDGE('',*,*,#2126,.F.);
#2810=ORIENTED_EDGE('',*,*,#2038,.T.);
#2811=ORIENTED_EDGE('',*,*,#2111,.T.);
#2812=ORIENTED_EDGE('',*,*,#2032,.T.);
#2813=ORIENTED_EDGE('',*,*,#2127,.F.);
#2814=ORIENTED_EDGE('',*,*,#2034,.T.);
#2815=ORIENTED_EDGE('',*,*,#2128,.F.);
#2816=ORIENTED_EDGE('',*,*,#2115,.T.);
#2817=ORIENTED_EDGE('',*,*,#2003,.T.);
#2818=ORIENTED_EDGE('',*,*,#2094,.T.);
#2819=ORIENTED_EDGE('',*,*,#2063,.T.);
#2820=ORIENTED_EDGE('',*,*,#2129,.F.);
#2821=ORIENTED_EDGE('',*,*,#1999,.T.);
#2822=ORIENTED_EDGE('',*,*,#2098,.T.);
#2823=ORIENTED_EDGE('',*,*,#2067,.T.);
#2824=ORIENTED_EDGE('',*,*,#2130,.F.);
#2825=ORIENTED_EDGE('',*,*,#1995,.T.);
#2826=ORIENTED_EDGE('',*,*,#2102,.T.);
#2827=ORIENTED_EDGE('',*,*,#2071,.T.);
#2828=ORIENTED_EDGE('',*,*,#2131,.F.);
#2829=ORIENTED_EDGE('',*,*,#1991,.T.);
#2830=ORIENTED_EDGE('',*,*,#2106,.T.);
#2831=ORIENTED_EDGE('',*,*,#2075,.T.);
#2832=ORIENTED_EDGE('',*,*,#2132,.F.);
#2833=ORIENTED_EDGE('',*,*,#1987,.T.);
#2834=ORIENTED_EDGE('',*,*,#2110,.T.);
#2835=ORIENTED_EDGE('',*,*,#2079,.T.);
#2836=ORIENTED_EDGE('',*,*,#2133,.F.);
#2837=ORIENTED_EDGE('',*,*,#1983,.T.);
#2838=ORIENTED_EDGE('',*,*,#2114,.T.);
#2839=ORIENTED_EDGE('',*,*,#2083,.T.);
#2840=ORIENTED_EDGE('',*,*,#2134,.F.);
#2841=ORIENTED_EDGE('',*,*,#2007,.T.);
#2842=ORIENTED_EDGE('',*,*,#2090,.T.);
#2843=ORIENTED_EDGE('',*,*,#2135,.T.);
#2844=ORIENTED_EDGE('',*,*,#2060,.T.);
#2845=ORIENTED_EDGE('',*,*,#2136,.T.);
#2846=ORIENTED_EDGE('',*,*,#2120,.T.);
#2847=ORIENTED_EDGE('',*,*,#2059,.T.);
#2848=ORIENTED_EDGE('',*,*,#2121,.T.);
#2849=ORIENTED_EDGE('',*,*,#2136,.F.);
#2850=ORIENTED_EDGE('',*,*,#2086,.T.);
#2851=ORIENTED_EDGE('',*,*,#2137,.T.);
#2852=ORIENTED_EDGE('',*,*,#2138,.F.);
#2853=ORIENTED_EDGE('',*,*,#2118,.T.);
#2854=ORIENTED_EDGE('',*,*,#2004,.T.);
#2855=ORIENTED_EDGE('',*,*,#2129,.T.);
#2856=ORIENTED_EDGE('',*,*,#2062,.T.);
#2857=ORIENTED_EDGE('',*,*,#2139,.T.);
#2858=ORIENTED_EDGE('',*,*,#2011,.T.);
#2859=ORIENTED_EDGE('',*,*,#2140,.T.);
#2860=ORIENTED_EDGE('',*,*,#2055,.T.);
#2861=ORIENTED_EDGE('',*,*,#2122,.T.);
#2862=ORIENTED_EDGE('',*,*,#2000,.T.);
#2863=ORIENTED_EDGE('',*,*,#2130,.T.);
#2864=ORIENTED_EDGE('',*,*,#2066,.T.);
#2865=ORIENTED_EDGE('',*,*,#2141,.T.);
#2866=ORIENTED_EDGE('',*,*,#2015,.T.);
#2867=ORIENTED_EDGE('',*,*,#2142,.T.);
#2868=ORIENTED_EDGE('',*,*,#2051,.T.);
#2869=ORIENTED_EDGE('',*,*,#2123,.T.);
#2870=ORIENTED_EDGE('',*,*,#1996,.T.);
#2871=ORIENTED_EDGE('',*,*,#2131,.T.);
#2872=ORIENTED_EDGE('',*,*,#2070,.T.);
#2873=ORIENTED_EDGE('',*,*,#2143,.T.);
#2874=ORIENTED_EDGE('',*,*,#2019,.T.);
#2875=ORIENTED_EDGE('',*,*,#2144,.T.);
#2876=ORIENTED_EDGE('',*,*,#2047,.T.);
#2877=ORIENTED_EDGE('',*,*,#2124,.T.);
#2878=ORIENTED_EDGE('',*,*,#1992,.T.);
#2879=ORIENTED_EDGE('',*,*,#2132,.T.);
#2880=ORIENTED_EDGE('',*,*,#2074,.T.);
#2881=ORIENTED_EDGE('',*,*,#2145,.T.);
#2882=ORIENTED_EDGE('',*,*,#2023,.T.);
#2883=ORIENTED_EDGE('',*,*,#2146,.T.);
#2884=ORIENTED_EDGE('',*,*,#2043,.T.);
#2885=ORIENTED_EDGE('',*,*,#2125,.T.);
#2886=ORIENTED_EDGE('',*,*,#1988,.T.);
#2887=ORIENTED_EDGE('',*,*,#2133,.T.);
#2888=ORIENTED_EDGE('',*,*,#2078,.T.);
#2889=ORIENTED_EDGE('',*,*,#2147,.T.);
#2890=ORIENTED_EDGE('',*,*,#2027,.T.);
#2891=ORIENTED_EDGE('',*,*,#2148,.T.);
#2892=ORIENTED_EDGE('',*,*,#2039,.T.);
#2893=ORIENTED_EDGE('',*,*,#2126,.T.);
#2894=ORIENTED_EDGE('',*,*,#1984,.T.);
#2895=ORIENTED_EDGE('',*,*,#2134,.T.);
#2896=ORIENTED_EDGE('',*,*,#2082,.T.);
#2897=ORIENTED_EDGE('',*,*,#2149,.T.);
#2898=ORIENTED_EDGE('',*,*,#2031,.T.);
#2899=ORIENTED_EDGE('',*,*,#2150,.T.);
#2900=ORIENTED_EDGE('',*,*,#2035,.T.);
#2901=ORIENTED_EDGE('',*,*,#2127,.T.);
#2902=ORIENTED_EDGE('',*,*,#2010,.T.);
#2903=ORIENTED_EDGE('',*,*,#2092,.F.);
#2904=ORIENTED_EDGE('',*,*,#2056,.T.);
#2905=ORIENTED_EDGE('',*,*,#2140,.F.);
#2906=ORIENTED_EDGE('',*,*,#2014,.T.);
#2907=ORIENTED_EDGE('',*,*,#2096,.F.);
#2908=ORIENTED_EDGE('',*,*,#2052,.T.);
#2909=ORIENTED_EDGE('',*,*,#2142,.F.);
#2910=ORIENTED_EDGE('',*,*,#2018,.T.);
#2911=ORIENTED_EDGE('',*,*,#2100,.F.);
#2912=ORIENTED_EDGE('',*,*,#2048,.T.);
#2913=ORIENTED_EDGE('',*,*,#2144,.F.);
#2914=ORIENTED_EDGE('',*,*,#2022,.T.);
#2915=ORIENTED_EDGE('',*,*,#2104,.F.);
#2916=ORIENTED_EDGE('',*,*,#2044,.T.);
#2917=ORIENTED_EDGE('',*,*,#2146,.F.);
#2918=ORIENTED_EDGE('',*,*,#2026,.T.);
#2919=ORIENTED_EDGE('',*,*,#2108,.F.);
#2920=ORIENTED_EDGE('',*,*,#2040,.T.);
#2921=ORIENTED_EDGE('',*,*,#2148,.F.);
#2922=ORIENTED_EDGE('',*,*,#2030,.T.);
#2923=ORIENTED_EDGE('',*,*,#2112,.F.);
#2924=ORIENTED_EDGE('',*,*,#2036,.T.);
#2925=ORIENTED_EDGE('',*,*,#2150,.F.);
#2926=ORIENTED_EDGE('',*,*,#2005,.T.);
#2927=ORIENTED_EDGE('',*,*,#2139,.F.);
#2928=ORIENTED_EDGE('',*,*,#2061,.T.);
#2929=ORIENTED_EDGE('',*,*,#2135,.F.);
#2930=ORIENTED_EDGE('',*,*,#2089,.F.);
#2931=ORIENTED_EDGE('',*,*,#2001,.T.);
#2932=ORIENTED_EDGE('',*,*,#2141,.F.);
#2933=ORIENTED_EDGE('',*,*,#2065,.T.);
#2934=ORIENTED_EDGE('',*,*,#2093,.F.);
#2935=ORIENTED_EDGE('',*,*,#1997,.T.);
#2936=ORIENTED_EDGE('',*,*,#2143,.F.);
#2937=ORIENTED_EDGE('',*,*,#2069,.T.);
#2938=ORIENTED_EDGE('',*,*,#2097,.F.);
#2939=ORIENTED_EDGE('',*,*,#1993,.T.);
#2940=ORIENTED_EDGE('',*,*,#2145,.F.);
#2941=ORIENTED_EDGE('',*,*,#2073,.T.);
#2942=ORIENTED_EDGE('',*,*,#2101,.F.);
#2943=ORIENTED_EDGE('',*,*,#1989,.T.);
#2944=ORIENTED_EDGE('',*,*,#2147,.F.);
#2945=ORIENTED_EDGE('',*,*,#2077,.T.);
#2946=ORIENTED_EDGE('',*,*,#2105,.F.);
#2947=ORIENTED_EDGE('',*,*,#1985,.T.);
#2948=ORIENTED_EDGE('',*,*,#2149,.F.);
#2949=ORIENTED_EDGE('',*,*,#2081,.T.);
#2950=ORIENTED_EDGE('',*,*,#2109,.F.);
#2951=ORIENTED_EDGE('',*,*,#1981,.T.);
#2952=ORIENTED_EDGE('',*,*,#2151,.F.);
#2953=ORIENTED_EDGE('',*,*,#2137,.F.);
#2954=ORIENTED_EDGE('',*,*,#2085,.T.);
#2955=ORIENTED_EDGE('',*,*,#2113,.F.);
#2956=ORIENTED_EDGE('',*,*,#1979,.T.);
#2957=ORIENTED_EDGE('',*,*,#2117,.F.);
#2958=ORIENTED_EDGE('',*,*,#2152,.F.);
#2959=ORIENTED_EDGE('',*,*,#2153,.F.);
#2960=ORIENTED_EDGE('',*,*,#2154,.T.);
#2961=ORIENTED_EDGE('',*,*,#2155,.F.);
#2962=ORIENTED_EDGE('',*,*,#2154,.F.);
#2963=ORIENTED_EDGE('',*,*,#2155,.T.);
#2964=ORIENTED_EDGE('',*,*,#2152,.T.);
#2965=ORIENTED_EDGE('',*,*,#2116,.T.);
#2966=ORIENTED_EDGE('',*,*,#2128,.T.);
#2967=ORIENTED_EDGE('',*,*,#2088,.F.);
#2968=ORIENTED_EDGE('',*,*,#2119,.T.);
#2969=ORIENTED_EDGE('',*,*,#2138,.T.);
#2970=ORIENTED_EDGE('',*,*,#2151,.T.);
#2971=ORIENTED_EDGE('',*,*,#1980,.F.);
#2972=ORIENTED_EDGE('',*,*,#2153,.T.);
#3579=B_SPLINE_SURFACE_WITH_KNOTS('',3,3,((#6564,#6565,#6566,#6567),(#6568,
#6569,#6570,#6571),(#6572,#6573,#6574,#6575),(#6576,#6577,#6578,#6579)),
 .UNSPECIFIED.,.F.,.F.,.F.,(4,4),(4,4),(0.066620174713851,0.0820126057383863),
(8.314732749858,8.70158673567856),.UNSPECIFIED.);
#3580=B_SPLINE_SURFACE_WITH_KNOTS('',3,3,((#6586,#6587,#6588,#6589,#6590,
#6591),(#6592,#6593,#6594,#6595,#6596,#6597),(#6598,#6599,#6600,#6601,#6602,
#6603),(#6604,#6605,#6606,#6607,#6608,#6609)),.UNSPECIFIED.,.F.,.F.,.F.,
(4,4),(4,1,1,4),(-0.000200320262106561,0.0820126057383863),(47.6103505270742,
48.3332993342991,49.0560729269844,49.7790217342094),.UNSPECIFIED.);
#3581=B_SPLINE_SURFACE_WITH_KNOTS('',3,3,((#6665,#6666,#6667,#6668,#6669,
#6670),(#6671,#6672,#6673,#6674,#6675,#6676),(#6677,#6678,#6679,#6680,#6681,
#6682),(#6683,#6684,#6685,#6686,#6687,#6688)),.UNSPECIFIED.,.F.,.F.,.F.,
(4,4),(4,1,1,4),(-0.000197985600878005,0.0820126057383863),(41.3271643941354,
42.0501140271196,42.7728876198048,43.495837252789),.UNSPECIFIED.);
#3582=B_SPLINE_SURFACE_WITH_KNOTS('',3,3,((#6695,#6696,#6697,#6698,#6699,
#6700),(#6701,#6702,#6703,#6704,#6705,#6706),(#6707,#6708,#6709,#6710,#6711,
#6712),(#6713,#6714,#6715,#6716,#6717,#6718)),.UNSPECIFIED.,.F.,.F.,.F.,
(4,4),(4,1,1,4),(-0.000195813814893523,0.0820126057383863),(35.0439783465439,
35.76692871994,36.4897023126252,37.2126526860213),.UNSPECIFIED.);
#3583=B_SPLINE_SURFACE_WITH_KNOTS('',3,3,((#6725,#6726,#6727,#6728,#6729,
#6730),(#6731,#6732,#6733,#6734,#6735,#6736),(#6737,#6738,#6739,#6740,#6741,
#6742),(#6743,#6744,#6745,#6746,#6747,#6748)),.UNSPECIFIED.,.F.,.F.,.F.,
(4,4),(4,1,1,4),(-0.000193785406214375,0.0820126057383863),(28.7607923707967,
29.4837434127604,30.2065170054456,30.9294680474093),.UNSPECIFIED.);
#3584=B_SPLINE_SURFACE_WITH_KNOTS('',3,3,((#6755,#6756,#6757,#6758,#6759,
#6760),(#6761,#6762,#6763,#6764,#6765,#6766),(#6767,#6768,#6769,#6770,#6771,
#6772),(#6773,#6774,#6775,#6776,#6777,#6778)),.UNSPECIFIED.,.F.,.F.,.F.,
(4,4),(4,1,1,4),(-0.000191884308595516,0.0820126057383863),(22.4776064561872,
23.2005581055808,23.9233316982661,24.6462833476596),.UNSPECIFIED.);
#3585=B_SPLINE_SURFACE_WITH_KNOTS('',3,3,((#6785,#6786,#6787,#6788,#6789,
#6790),(#6791,#6792,#6793,#6794,#6795,#6796),(#6797,#6798,#6799,#6800,#6801,
#6802),(#6803,#6804,#6805,#6806,#6807,#6808)),.UNSPECIFIED.,.F.,.F.,.F.,
(4,4),(4,1,1,4),(-0.000190097099794286,0.0820126057383863),(16.1944205941067,
16.9173727984012,17.6401463910865,18.363098595381),.UNSPECIFIED.);
#3586=B_SPLINE_SURFACE_WITH_KNOTS('',3,3,((#6815,#6816,#6817,#6818,#6819,
#6820),(#6821,#6822,#6823,#6824,#6825,#6826),(#6827,#6828,#6829,#6830,#6831,
#6832),(#6833,#6834,#6835,#6836,#6837,#6838)),.UNSPECIFIED.,.F.,.F.,.F.,
(4,4),(4,1,1,4),(-0.000156396744294902,0.0821188966323171),(9.98287940740301,
10.6818311637994,11.3807829201958,12.0798910733364),.UNSPECIFIED.);
#3587=B_SPLINE_SURFACE_WITH_KNOTS('',3,3,((#6907,#6908,#6909,#6910,#6911,
#6912),(#6913,#6914,#6915,#6916,#6917,#6918),(#6919,#6920,#6921,#6922,#6923,
#6924),(#6925,#6926,#6927,#6928,#6929,#6930)),.UNSPECIFIED.,.F.,.F.,.F.,
(4,4),(4,1,1,4),(-0.000199131191863258,0.0820126057383863),(44.4687574489585,
45.1917066807094,45.9144802733946,46.6374295051455),.UNSPECIFIED.);
#3588=B_SPLINE_SURFACE_WITH_KNOTS('',3,3,((#6937,#6938,#6939,#6940,#6941,
#6942),(#6943,#6944,#6945,#6946,#6947,#6948),(#6949,#6950,#6951,#6952,#6953,
#6954),(#6955,#6956,#6957,#6958,#6959,#6960)),.UNSPECIFIED.,.F.,.F.,.F.,
(4,4),(4,1,1,4),(-0.000196880658646492,0.0820126057383863),(38.1855713605906,
38.9085213735298,39.631294966215,40.3542449791542),.UNSPECIFIED.);
#3589=B_SPLINE_SURFACE_WITH_KNOTS('',3,3,((#6967,#6968,#6969,#6970,#6971,
#6972),(#6973,#6974,#6975,#6976,#6977,#6978),(#6979,#6980,#6981,#6982,#6983,
#6984),(#6985,#6986,#6987,#6988,#6989,#6990)),.UNSPECIFIED.,.F.,.F.,.F.,
(4,4),(4,1,1,4),(-0.000194782762460684,0.0820126057383863),(31.9023853504151,
32.6253360663502,33.3481096590354,34.0710603749705),.UNSPECIFIED.);
#3590=B_SPLINE_SURFACE_WITH_KNOTS('',3,3,((#6997,#6998,#6999,#7000,#7001,
#7002),(#7003,#7004,#7005,#7006,#7007,#7008),(#7009,#7010,#7011,#7012,#7013,
#7014),(#7015,#7016,#7017,#7018,#7019,#7020)),.UNSPECIFIED.,.F.,.F.,.F.,
(4,4),(4,1,1,4),(-0.000192819836832936,0.0820126057383863),(25.6191994064303,
26.3421507591706,27.0649243518558,27.7878757045961),.UNSPECIFIED.);
#3591=B_SPLINE_SURFACE_WITH_KNOTS('',3,3,((#7027,#7028,#7029,#7030,#7031,
#7032),(#7033,#7034,#7035,#7036,#7037,#7038),(#7039,#7040,#7041,#7042,#7043,
#7044),(#7045,#7046,#7047,#7048,#7049,#7050)),.UNSPECIFIED.,.F.,.F.,.F.,
(4,4),(4,1,1,4),(-0.000190977220451414,0.0820126057383863),(19.3360135190516,
20.058965451991,20.7817390446763,21.5046909776157),.UNSPECIFIED.);
#3592=B_SPLINE_SURFACE_WITH_KNOTS('',3,3,((#7057,#7058,#7059,#7060,#7061,
#7062),(#7063,#7064,#7065,#7066,#7067,#7068),(#7069,#7070,#7071,#7072,#7073,
#7074),(#7075,#7076,#7077,#7078,#7079,#7080)),.UNSPECIFIED.,.F.,.F.,.F.,
(4,4),(4,1,1,4),(-0.000189242588512825,0.0820126057383863),(13.0528276805227,
13.7757801448114,14.4985537374967,15.2215062017854),.UNSPECIFIED.);
#3593=B_SPLINE_SURFACE_WITH_KNOTS('',3,3,((#7281,#7282,#7283,#7284,#7285,
#7286),(#7287,#7288,#7289,#7290,#7291,#7292),(#7293,#7294,#7295,#7296,#7297,
#7298),(#7299,#7300,#7301,#7302,#7303,#7304)),.UNSPECIFIED.,.F.,.F.,.F.,
(4,4),(4,1,1,4),(0.,0.0822109230065992),(47.6103498167155,48.3332993342991,
49.0560729269844,49.7790224445681),.UNSPECIFIED.);
#3594=B_SPLINE_SURFACE_WITH_KNOTS('',3,3,((#7305,#7306,#7307,#7308,#7309,
#7310),(#7311,#7312,#7313,#7314,#7315,#7316),(#7317,#7318,#7319,#7320,#7321,
#7322),(#7323,#7324,#7325,#7326,#7327,#7328)),.UNSPECIFIED.,.F.,.F.,.F.,
(4,4),(4,1,1,4),(0.,0.0822087286475259),(41.3271637575297,42.0501140271195,
42.7728876198048,43.4958378893947),.UNSPECIFIED.);
#3595=B_SPLINE_SURFACE_WITH_KNOTS('',3,3,((#7329,#7330,#7331,#7332,#7333,
#7334),(#7335,#7336,#7337,#7338,#7339,#7340),(#7341,#7342,#7343,#7344,#7345,
#7346),(#7347,#7348,#7349,#7350,#7351,#7352)),.UNSPECIFIED.,.F.,.F.,.F.,
(4,4),(4,1,1,4),(0.,0.0822066802882628),(35.0439777719737,35.76692871994,
36.4897023126252,37.2126532605915),.UNSPECIFIED.);
#3596=B_SPLINE_SURFACE_WITH_KNOTS('',3,3,((#7353,#7354,#7355,#7356,#7357,
#7358),(#7359,#7360,#7361,#7362,#7363,#7364),(#7365,#7366,#7367,#7368,#7369,
#7370),(#7371,#7372,#7373,#7374,#7375,#7376)),.UNSPECIFIED.,.F.,.F.,.F.,
(4,4),(4,1,1,4),(0.,0.0822047614148872),(28.7607918489802,29.4837434127604,
30.2065170054456,30.9294685692258),.UNSPECIFIED.);
#3597=B_SPLINE_SURFACE_WITH_KNOTS('',3,3,((#7377,#7378,#7379,#7380,#7381,
#7382),(#7383,#7384,#7385,#7386,#7387,#7388),(#7389,#7390,#7391,#7392,#7393,
#7394),(#7395,#7396,#7397,#7398,#7399,#7400)),.UNSPECIFIED.,.F.,.F.,.F.,
(4,4),(4,1,1,4),(0.,0.0822029582573803),(22.4776059796679,23.2005581055808,
23.9233316982661,24.6462838241789),.UNSPECIFIED.);
#3598=B_SPLINE_SURFACE_WITH_KNOTS('',3,3,((#7401,#7402,#7403,#7404,#7405,
#7406),(#7407,#7408,#7409,#7410,#7411,#7412),(#7413,#7414,#7415,#7416,#7417,
#7418),(#7419,#7420,#7421,#7422,#7423,#7424)),.UNSPECIFIED.,.F.,.F.,.F.,
(4,4),(4,1,1,4),(0.,0.082201259192146),(16.1944201568192,16.9173727984012,
17.6401463910865,18.3630990326685),.UNSPECIFIED.);
#3599=B_SPLINE_SURFACE_WITH_KNOTS('',3,3,((#7425,#7426,#7427,#7428,#7429,
#7430),(#7431,#7432,#7433,#7434,#7435,#7436),(#7437,#7438,#7439,#7440,#7441,
#7442),(#7443,#7444,#7445,#7446,#7447,#7448)),.UNSPECIFIED.,.F.,.F.,.F.,
(4,4),(4,1,1,4),(-9.65518509377315E-5,0.0821438972802576),(50.7519871036618,
51.4243296588263,52.0965409224489,52.7687521860715),.UNSPECIFIED.);
#3600=B_SPLINE_SURFACE_WITH_KNOTS('',3,3,((#7449,#7450,#7451,#7452,#7453,
#7454),(#7455,#7456,#7457,#7458,#7459,#7460),(#7461,#7462,#7463,#7464,#7465,
#7466),(#7467,#7468,#7469,#7470,#7471,#7472)),.UNSPECIFIED.,.F.,.F.,.F.,
(4,4),(4,1,1,4),(0.,0.08220980641716),(44.4687567771236,45.1917066807094,
45.9144802733946,46.6374301769804),.UNSPECIFIED.);
#3601=B_SPLINE_SURFACE_WITH_KNOTS('',3,3,((#7473,#7474,#7475,#7476,#7477,
#7478),(#7479,#7480,#7481,#7482,#7483,#7484),(#7485,#7486,#7487,#7488,#7489,
#7490),(#7491,#7492,#7493,#7494,#7495,#7496)),.UNSPECIFIED.,.F.,.F.,.F.,
(4,4),(4,1,1,4),(0.,0.0822076873226976),(38.1855707562983,38.9085213735298,
39.631294966215,40.3542455834465),.UNSPECIFIED.);
#3602=B_SPLINE_SURFACE_WITH_KNOTS('',3,3,((#7497,#7498,#7499,#7500,#7501,
#7502),(#7503,#7504,#7505,#7506,#7507,#7508),(#7509,#7510,#7511,#7512,#7513,
#7514),(#7515,#7516,#7517,#7518,#7519,#7520)),.UNSPECIFIED.,.F.,.F.,.F.,
(4,4),(4,1,1,4),(0.,0.0822057055828623),(31.902384803256,32.6253360663502,
33.3481096590354,34.0710609221296),.UNSPECIFIED.);
#3603=B_SPLINE_SURFACE_WITH_KNOTS('',3,3,((#7521,#7522,#7523,#7524,#7525,
#7526),(#7527,#7528,#7529,#7530,#7531,#7532),(#7533,#7534,#7535,#7536,#7537,
#7538),(#7539,#7540,#7541,#7542,#7543,#7544)),.UNSPECIFIED.,.F.,.F.,.F.,
(4,4),(4,1,1,4),(0.,0.0822038461426398),(25.619198908099,26.3421507591706,
27.0649243518559,27.7878762029274),.UNSPECIFIED.);
#3604=B_SPLINE_SURFACE_WITH_KNOTS('',3,3,((#7545,#7546,#7547,#7548,#7549,
#7550),(#7551,#7552,#7553,#7554,#7555,#7556),(#7557,#7558,#7559,#7560,#7561,
#7562),(#7563,#7564,#7565,#7566,#7567,#7568)),.UNSPECIFIED.,.F.,.F.,.F.,
(4,4),(4,1,1,4),(0.,0.0822020963687411),(19.3360130628329,20.058965451991,
20.7817390446763,21.5046914338344),.UNSPECIFIED.);
#3605=B_SPLINE_SURFACE_WITH_KNOTS('',3,3,((#7569,#7570,#7571,#7572,#7573,
#7574),(#7575,#7576,#7577,#7578,#7579,#7580),(#7581,#7582,#7583,#7584,#7585,
#7586),(#7587,#7588,#7589,#7590,#7591,#7592)),.UNSPECIFIED.,.F.,.F.,.F.,
(4,4),(4,1,1,4),(0.,0.0822004455378898),(13.0528272609226,13.7757801448114,
14.4985537374967,15.2215066213855),.UNSPECIFIED.);
#3606=B_SPLINE_SURFACE_WITH_KNOTS('',3,3,((#7594,#7595,#7596,#7597),(#7598,
#7599,#7600,#7601),(#7602,#7603,#7604,#7605),(#7606,#7607,#7608,#7609)),
 .UNSPECIFIED.,.F.,.F.,.F.,(4,4),(4,4),(0.0663734465876268,0.0820126057383863),
(11.6152142277547,12.0797346765921),.UNSPECIFIED.);
#3648=ADVANCED_FACE('',(#473),#183,.F.);
#3649=ADVANCED_FACE('',(#474),#184,.F.);
#3650=ADVANCED_FACE('',(#475),#353,.T.);
#3651=ADVANCED_FACE('',(#476),#354,.T.);
#3652=ADVANCED_FACE('',(#477),#355,.T.);
#3653=ADVANCED_FACE('',(#478),#356,.T.);
#3654=ADVANCED_FACE('',(#479),#357,.T.);
#3655=ADVANCED_FACE('',(#480),#358,.T.);
#3656=ADVANCED_FACE('',(#481),#359,.T.);
#3657=ADVANCED_FACE('',(#482),#360,.T.);
#3658=ADVANCED_FACE('',(#483),#361,.T.);
#3659=ADVANCED_FACE('',(#484),#362,.T.);
#3660=ADVANCED_FACE('',(#485),#363,.T.);
#3661=ADVANCED_FACE('',(#486),#364,.T.);
#3662=ADVANCED_FACE('',(#487),#365,.T.);
#3663=ADVANCED_FACE('',(#488),#366,.T.);
#3664=ADVANCED_FACE('',(#489),#3579,.F.);
#3665=ADVANCED_FACE('',(#490),#3580,.F.);
#3666=ADVANCED_FACE('',(#491),#3581,.F.);
#3667=ADVANCED_FACE('',(#492),#3582,.F.);
#3668=ADVANCED_FACE('',(#493),#3583,.F.);
#3669=ADVANCED_FACE('',(#494),#3584,.F.);
#3670=ADVANCED_FACE('',(#495),#3585,.F.);
#3671=ADVANCED_FACE('',(#496),#3586,.F.);
#3672=ADVANCED_FACE('',(#497),#3587,.F.);
#3673=ADVANCED_FACE('',(#498),#3588,.F.);
#3674=ADVANCED_FACE('',(#499),#3589,.F.);
#3675=ADVANCED_FACE('',(#500),#3590,.F.);
#3676=ADVANCED_FACE('',(#501),#3591,.F.);
#3677=ADVANCED_FACE('',(#502),#3592,.F.);
#3678=ADVANCED_FACE('',(#503),#185,.T.);
#3679=ADVANCED_FACE('',(#504),#367,.T.);
#3680=ADVANCED_FACE('',(#505),#368,.T.);
#3681=ADVANCED_FACE('',(#506),#369,.T.);
#3682=ADVANCED_FACE('',(#507),#370,.T.);
#3683=ADVANCED_FACE('',(#508),#371,.T.);
#3684=ADVANCED_FACE('',(#509),#372,.T.);
#3685=ADVANCED_FACE('',(#510),#373,.T.);
#3686=ADVANCED_FACE('',(#511),#374,.T.);
#3687=ADVANCED_FACE('',(#512),#375,.T.);
#3688=ADVANCED_FACE('',(#513),#376,.T.);
#3689=ADVANCED_FACE('',(#514),#377,.T.);
#3690=ADVANCED_FACE('',(#515),#378,.T.);
#3691=ADVANCED_FACE('',(#516),#379,.T.);
#3692=ADVANCED_FACE('',(#517),#380,.T.);
#3693=ADVANCED_FACE('',(#518),#3593,.F.);
#3694=ADVANCED_FACE('',(#519),#3594,.F.);
#3695=ADVANCED_FACE('',(#520),#3595,.F.);
#3696=ADVANCED_FACE('',(#521),#3596,.F.);
#3697=ADVANCED_FACE('',(#522),#3597,.F.);
#3698=ADVANCED_FACE('',(#523),#3598,.F.);
#3699=ADVANCED_FACE('',(#524),#3599,.F.);
#3700=ADVANCED_FACE('',(#525),#3600,.F.);
#3701=ADVANCED_FACE('',(#526),#3601,.F.);
#3702=ADVANCED_FACE('',(#527),#3602,.F.);
#3703=ADVANCED_FACE('',(#528),#3603,.F.);
#3704=ADVANCED_FACE('',(#529),#3604,.F.);
#3705=ADVANCED_FACE('',(#530),#3605,.F.);
#3706=ADVANCED_FACE('',(#531),#3606,.F.);
#3707=ADVANCED_FACE('',(#532),#381,.T.);
#3708=ADVANCED_FACE('',(#533,#138),#186,.T.);
#3709=ADVANCED_FACE('',(#534),#187,.F.);
#3837=CLOSED_SHELL('',(#3648,#3649,#3650,#3651,#3652,#3653,#3654,#3655,
#3656,#3657,#3658,#3659,#3660,#3661,#3662,#3663,#3664,#3665,#3666,#3667,
#3668,#3669,#3670,#3671,#3672,#3673,#3674,#3675,#3676,#3677,#3678,#3679,
#3680,#3681,#3682,#3683,#3684,#3685,#3686,#3687,#3688,#3689,#3690,#3691,
#3692,#3693,#3694,#3695,#3696,#3697,#3698,#3699,#3700,#3701,#3702,#3703,
#3704,#3705,#3706,#3707,#3708,#3709));
#4008=AXIS2_PLACEMENT_3D('',#5584,#4445,#4446);
#4009=AXIS2_PLACEMENT_3D('',#5585,#4447,#4448);
#4010=AXIS2_PLACEMENT_3D('',#5881,#4477,#4478);
#4011=AXIS2_PLACEMENT_3D('',#6177,#4507,#4508);
#4012=AXIS2_PLACEMENT_3D('',#6191,#4509,#4510);
#4013=AXIS2_PLACEMENT_3D('',#6192,#4511,#4512);
#4014=AXIS2_PLACEMENT_3D('',#6221,#4513,#4514);
#4015=AXIS2_PLACEMENT_3D('',#6250,#4515,#4516);
#4016=AXIS2_PLACEMENT_3D('',#6279,#4517,#4518);
#4017=AXIS2_PLACEMENT_3D('',#6308,#4519,#4520);
#4018=AXIS2_PLACEMENT_3D('',#6337,#4521,#4522);
#4019=AXIS2_PLACEMENT_3D('',#6366,#4523,#4524);
#4020=AXIS2_PLACEMENT_3D('',#6395,#4525,#4526);
#4021=AXIS2_PLACEMENT_3D('',#6424,#4527,#4528);
#4022=AXIS2_PLACEMENT_3D('',#6453,#4529,#4530);
#4023=AXIS2_PLACEMENT_3D('',#6482,#4531,#4532);
#4024=AXIS2_PLACEMENT_3D('',#6511,#4533,#4534);
#4025=AXIS2_PLACEMENT_3D('',#6540,#4535,#4536);
#4026=AXIS2_PLACEMENT_3D('',#6557,#4537,#4538);
#4027=AXIS2_PLACEMENT_3D('',#6585,#4539,#4540);
#4028=AXIS2_PLACEMENT_3D('',#6906,#4541,#4542);
#4029=AXIS2_PLACEMENT_3D('',#7087,#4543,#4544);
#4030=AXIS2_PLACEMENT_3D('',#7131,#4545,#4546);
#4031=AXIS2_PLACEMENT_3D('',#7132,#4547,#4548);
#4032=AXIS2_PLACEMENT_3D('',#7133,#4549,#4550);
#4033=AXIS2_PLACEMENT_3D('',#7141,#4551,#4552);
#4034=AXIS2_PLACEMENT_3D('',#7142,#4553,#4554);
#4035=AXIS2_PLACEMENT_3D('',#7204,#4555,#4556);
#4036=AXIS2_PLACEMENT_3D('',#7211,#4557,#4558);
#4037=AXIS2_PLACEMENT_3D('',#7218,#4559,#4560);
#4038=AXIS2_PLACEMENT_3D('',#7225,#4561,#4562);
#4039=AXIS2_PLACEMENT_3D('',#7232,#4563,#4564);
#4040=AXIS2_PLACEMENT_3D('',#7239,#4565,#4566);
#4041=AXIS2_PLACEMENT_3D('',#7246,#4567,#4568);
#4042=AXIS2_PLACEMENT_3D('',#7253,#4569,#4570);
#4043=AXIS2_PLACEMENT_3D('',#7260,#4571,#4572);
#4044=AXIS2_PLACEMENT_3D('',#7267,#4573,#4574);
#4045=AXIS2_PLACEMENT_3D('',#7274,#4575,#4576);
#4046=AXIS2_PLACEMENT_3D('',#7593,#4577,#4578);
#4047=AXIS2_PLACEMENT_3D('',#7616,#4579,#4580);
#4048=AXIS2_PLACEMENT_3D('',#7618,#4581,#4582);
#4049=AXIS2_PLACEMENT_3D('',#7621,#4584,#4585);
#4050=AXIS2_PLACEMENT_3D('',#7622,#4586,#4587);
#4051=AXIS2_PLACEMENT_3D('',#7623,#4588,#4589);
#4445=DIRECTION('axis',(0.,0.,1.));
#4446=DIRECTION('refdir',(1.,0.,0.));
#4447=DIRECTION('center_axis',(0.,1.,0.));
#4448=DIRECTION('ref_axis',(0.,0.,1.));
#4449=DIRECTION('',(0.,0.,1.));
#4450=DIRECTION('',(1.,0.,0.));
#4451=DIRECTION('',(1.,0.,0.));
#4452=DIRECTION('',(1.,0.,0.));
#4453=DIRECTION('',(1.,0.,0.));
#4454=DIRECTION('',(1.,0.,0.));
#4455=DIRECTION('',(1.,0.,0.));
#4456=DIRECTION('',(1.,0.,0.));
#4457=DIRECTION('',(1.,0.,0.));
#4458=DIRECTION('',(1.,0.,0.));
#4459=DIRECTION('',(1.,0.,0.));
#4460=DIRECTION('',(1.,0.,0.));
#4461=DIRECTION('',(1.,0.,0.));
#4462=DIRECTION('',(1.,0.,0.));
#4463=DIRECTION('',(0.,0.,1.));
#4464=DIRECTION('',(-1.,0.,0.));
#4465=DIRECTION('',(-1.,0.,0.));
#4466=DIRECTION('',(-1.,0.,0.));
#4467=DIRECTION('',(-1.,0.,0.));
#4468=DIRECTION('',(-1.,0.,0.));
#4469=DIRECTION('',(-1.,0.,0.));
#4470=DIRECTION('',(-1.,0.,0.));
#4471=DIRECTION('',(-1.,0.,0.));
#4472=DIRECTION('',(-1.,0.,0.));
#4473=DIRECTION('',(-1.,0.,0.));
#4474=DIRECTION('',(-1.,0.,0.));
#4475=DIRECTION('',(-1.,0.,0.));
#4476=DIRECTION('',(-1.,0.,0.));
#4477=DIRECTION('center_axis',(0.,-1.,0.));
#4478=DIRECTION('ref_axis',(0.,0.,-1.));
#4479=DIRECTION('',(1.,0.,0.));
#4480=DIRECTION('',(1.,0.,0.));
#4481=DIRECTION('',(1.,0.,0.));
#4482=DIRECTION('',(1.,0.,0.));
#4483=DIRECTION('',(1.,0.,0.));
#4484=DIRECTION('',(1.,0.,0.));
#4485=DIRECTION('',(1.,0.,0.));
#4486=DIRECTION('',(1.,0.,0.));
#4487=DIRECTION('',(1.,0.,0.));
#4488=DIRECTION('',(1.,0.,0.));
#4489=DIRECTION('',(1.,0.,0.));
#4490=DIRECTION('',(1.,0.,0.));
#4491=DIRECTION('',(1.,0.,0.));
#4492=DIRECTION('',(0.,0.,-1.));
#4493=DIRECTION('',(-1.,0.,0.));
#4494=DIRECTION('',(-1.,0.,0.));
#4495=DIRECTION('',(-1.,0.,0.));
#4496=DIRECTION('',(-1.,0.,0.));
#4497=DIRECTION('',(-1.,0.,0.));
#4498=DIRECTION('',(-1.,0.,0.));
#4499=DIRECTION('',(-1.,0.,0.));
#4500=DIRECTION('',(-1.,0.,0.));
#4501=DIRECTION('',(-1.,0.,0.));
#4502=DIRECTION('',(-1.,0.,0.));
#4503=DIRECTION('',(-1.,0.,0.));
#4504=DIRECTION('',(-1.,0.,0.));
#4505=DIRECTION('',(-1.,0.,0.));
#4506=DIRECTION('',(0.,0.,-1.));
#4507=DIRECTION('center_axis',(-1.,0.,0.));
#4508=DIRECTION('ref_axis',(0.,-1.,2.19773242311135E-14));
#4509=DIRECTION('center_axis',(-1.,0.,0.));
#4510=DIRECTION('ref_axis',(0.,-1.,2.19773242311135E-14));
#4511=DIRECTION('center_axis',(-1.,0.,0.));
#4512=DIRECTION('ref_axis',(0.,-1.,2.19773242311135E-14));
#4513=DIRECTION('center_axis',(-1.,0.,0.));
#4514=DIRECTION('ref_axis',(0.,-1.,2.19773242311135E-14));
#4515=DIRECTION('center_axis',(-1.,0.,0.));
#4516=DIRECTION('ref_axis',(0.,-1.,2.19773242311135E-14));
#4517=DIRECTION('center_axis',(-1.,0.,0.));
#4518=DIRECTION('ref_axis',(0.,-1.,2.19773242311135E-14));
#4519=DIRECTION('center_axis',(-1.,0.,0.));
#4520=DIRECTION('ref_axis',(0.,-1.,2.19773242311135E-14));
#4521=DIRECTION('center_axis',(-1.,0.,0.));
#4522=DIRECTION('ref_axis',(0.,-1.,2.19773242311135E-14));
#4523=DIRECTION('center_axis',(-1.,0.,0.));
#4524=DIRECTION('ref_axis',(0.,-1.,2.19773242311135E-14));
#4525=DIRECTION('center_axis',(-1.,0.,0.));
#4526=DIRECTION('ref_axis',(0.,-1.,2.19773242311135E-14));
#4527=DIRECTION('center_axis',(-1.,0.,0.));
#4528=DIRECTION('ref_axis',(0.,-1.,2.19773242311135E-14));
#4529=DIRECTION('center_axis',(-1.,0.,0.));
#4530=DIRECTION('ref_axis',(0.,-1.,2.19773242311135E-14));
#4531=DIRECTION('center_axis',(-1.,0.,0.));
#4532=DIRECTION('ref_axis',(0.,-1.,2.19773242311135E-14));
#4533=DIRECTION('center_axis',(-1.,0.,0.));
#4534=DIRECTION('ref_axis',(0.,-1.,2.19773242311135E-14));
#4535=DIRECTION('center_axis',(-1.,0.,0.));
#4536=DIRECTION('ref_axis',(0.,-1.,2.19773242311135E-14));
#4537=DIRECTION('center_axis',(1.,0.,0.));
#4538=DIRECTION('ref_axis',(0.,-1.,2.19773242311135E-14));
#4539=DIRECTION('center_axis',(1.,2.26944640896891E-13,2.4756931710509E-13));
#4540=DIRECTION('ref_axis',(-2.99635666187292E-14,0.794492776111595,-0.607273602840179));
#4541=DIRECTION('center_axis',(1.,-4.24721344664965E-14,7.81460509822211E-14));
#4542=DIRECTION('ref_axis',(-1.5231504897179E-14,0.783860772073074,0.620936623179052));
#4543=DIRECTION('center_axis',(-1.,0.,0.));
#4544=DIRECTION('ref_axis',(0.,-1.,0.));
#4545=DIRECTION('center_axis',(1.,0.,0.));
#4546=DIRECTION('ref_axis',(0.,-1.,0.));
#4547=DIRECTION('center_axis',(-1.,0.,0.));
#4548=DIRECTION('ref_axis',(0.,-1.,0.));
#4549=DIRECTION('center_axis',(-1.,0.,0.));
#4550=DIRECTION('ref_axis',(0.,-1.,0.));
#4551=DIRECTION('center_axis',(1.,0.,0.));
#4552=DIRECTION('ref_axis',(0.,-1.,0.));
#4553=DIRECTION('center_axis',(-1.,0.,0.));
#4554=DIRECTION('ref_axis',(0.,-1.,0.));
#4555=DIRECTION('center_axis',(-1.,0.,0.));
#4556=DIRECTION('ref_axis',(0.,-1.,0.));
#4557=DIRECTION('center_axis',(-1.,0.,0.));
#4558=DIRECTION('ref_axis',(0.,-1.,0.));
#4559=DIRECTION('center_axis',(-1.,0.,0.));
#4560=DIRECTION('ref_axis',(0.,-1.,0.));
#4561=DIRECTION('center_axis',(-1.,0.,0.));
#4562=DIRECTION('ref_axis',(0.,-1.,0.));
#4563=DIRECTION('center_axis',(-1.,0.,0.));
#4564=DIRECTION('ref_axis',(0.,-1.,0.));
#4565=DIRECTION('center_axis',(-1.,0.,0.));
#4566=DIRECTION('ref_axis',(0.,-1.,0.));
#4567=DIRECTION('center_axis',(-1.,0.,0.));
#4568=DIRECTION('ref_axis',(0.,-1.,0.));
#4569=DIRECTION('center_axis',(-1.,0.,0.));
#4570=DIRECTION('ref_axis',(0.,-1.,0.));
#4571=DIRECTION('center_axis',(-1.,0.,0.));
#4572=DIRECTION('ref_axis',(0.,-1.,0.));
#4573=DIRECTION('center_axis',(-1.,0.,0.));
#4574=DIRECTION('ref_axis',(0.,-1.,0.));
#4575=DIRECTION('center_axis',(-1.,0.,0.));
#4576=DIRECTION('ref_axis',(0.,-1.,0.));
#4577=DIRECTION('center_axis',(1.,-7.18663344203148E-15,1.44094323913819E-14));
#4578=DIRECTION('ref_axis',(-4.36221174028662E-15,0.74050159851997,0.672054597922944));
#4579=DIRECTION('center_axis',(1.,0.,0.));
#4580=DIRECTION('ref_axis',(0.,-1.,0.));
#4581=DIRECTION('center_axis',(1.,0.,0.));
#4582=DIRECTION('ref_axis',(0.,-1.,0.));
#4583=DIRECTION('',(-1.,0.,0.));
#4584=DIRECTION('center_axis',(-1.,0.,0.));
#4585=DIRECTION('ref_axis',(0.,-1.,0.));
#4586=DIRECTION('center_axis',(-1.,0.,0.));
#4587=DIRECTION('ref_axis',(0.,-1.,0.));
#4588=DIRECTION('center_axis',(-1.,0.,0.));
#4589=DIRECTION('ref_axis',(0.,-1.,0.));
#5584=CARTESIAN_POINT('',(0.,0.,0.));
#5585=CARTESIAN_POINT('Origin',(3.02384907614375,-2.84862442585767,-2.80808455720391));
#5586=CARTESIAN_POINT('',(11.0238443243108,-2.84860562949496,-1.77825041122887));
#5587=CARTESIAN_POINT('',(10.9314356691441,-2.84862442585767,-1.5071351773836));
#5588=CARTESIAN_POINT('Ctrl Pts',(11.0238395724777,-2.84862442585767,-1.77821291115482));
#5589=CARTESIAN_POINT('Ctrl Pts',(11.023058671384,-2.84862442585767,-1.77602158816867));
#5590=CARTESIAN_POINT('Ctrl Pts',(11.0222784621947,-2.84862442585824,-1.7738300165061));
#5591=CARTESIAN_POINT('Ctrl Pts',(11.0062774820837,-2.84862442585824,-1.72883879945583));
#5592=CARTESIAN_POINT('Ctrl Pts',(10.9913133628153,-2.84862442585851,-1.68592261376175));
#5593=CARTESIAN_POINT('Ctrl Pts',(10.9612482690896,-2.84862442585851,-1.59778423981652));
#5594=CARTESIAN_POINT('Ctrl Pts',(10.9461611622631,-2.84862442585767,-1.55250504487283));
#5595=CARTESIAN_POINT('Ctrl Pts',(10.9314356691441,-2.84862442585767,-1.5071351773836));
#5596=CARTESIAN_POINT('',(11.0238490787776,-2.84862442708621,2.51132611197218));
#5597=CARTESIAN_POINT('',(11.0238490761438,-2.84862442585767,6.75363122348402));
#5598=CARTESIAN_POINT('',(10.7378093816896,-2.84862442585767,1.50713517738359));
#5599=CARTESIAN_POINT('Ctrl Pts',(10.7378093816896,-2.84862442585767,1.5071351773836));
#5600=CARTESIAN_POINT('Ctrl Pts',(10.7745509100274,-2.84862442585767,1.67768015510688));
#5601=CARTESIAN_POINT('Ctrl Pts',(10.8181799183082,-2.84862442695797,1.84746530235002));
#5602=CARTESIAN_POINT('Ctrl Pts',(10.9144539328214,-2.84862442695797,2.18146463191032));
#5603=CARTESIAN_POINT('Ctrl Pts',(10.9675731917165,-2.84862442585767,2.34753476778138));
#5604=CARTESIAN_POINT('Ctrl Pts',(11.0238490840452,-2.84862442585767,2.51132611046758));
#5605=CARTESIAN_POINT('',(10.4912624831434,-2.84862442585767,1.50713517738358));
#5606=CARTESIAN_POINT('',(13.3346225254169,-2.84862442585767,1.50713517738359));
#5607=CARTESIAN_POINT('',(10.0266595508789,-2.8468189348389,2.71028906341842));
#5608=CARTESIAN_POINT('Ctrl Pts',(10.0267941012523,-2.84862442585767,2.70859765771964));
#5609=CARTESIAN_POINT('Ctrl Pts',(10.0337979544476,-2.84862442585767,2.69250499494907));
#5610=CARTESIAN_POINT('Ctrl Pts',(10.0407818720682,-2.84862442585767,2.67640214955592));
#5611=CARTESIAN_POINT('Ctrl Pts',(10.1253566086339,-2.84862442585767,2.48069385236447));
#5612=CARTESIAN_POINT('Ctrl Pts',(10.2012319741895,-2.84862442733188,2.29789169628234));
#5613=CARTESIAN_POINT('Ctrl Pts',(10.3504646709377,-2.84862442733188,1.91583275087761));
#5614=CARTESIAN_POINT('Ctrl Pts',(10.4249778185909,-2.84862442585767,1.7113610340671));
#5615=CARTESIAN_POINT('Ctrl Pts',(10.4912624831434,-2.84862442585767,1.5071351773836));
#5616=CARTESIAN_POINT('',(9.84333250807827,-2.84681996108769,2.71028970167779));
#5617=CARTESIAN_POINT('',(11.0238490761438,-2.84862442585767,2.71179421793157));
#5618=CARTESIAN_POINT('',(9.48780938168963,-2.84862442585767,1.50713517738359));
#5619=CARTESIAN_POINT('Ctrl Pts',(9.48780938168963,-2.84862442585767,1.5071351773836));
#5620=CARTESIAN_POINT('Ctrl Pts',(9.53185899985944,-2.84862442585767,1.71160247880986));
#5621=CARTESIAN_POINT('Ctrl Pts',(9.58587318685495,-2.84862442792121,1.91525078718682));
#5622=CARTESIAN_POINT('Ctrl Pts',(9.70094960223702,-2.84862442792121,2.2980896617317));
#5623=CARTESIAN_POINT('Ctrl Pts',(9.76180678295297,-2.84862442585767,2.48053952383311));
#5624=CARTESIAN_POINT('Ctrl Pts',(9.8318097489011,-2.84862442585767,2.67629614457399));
#5625=CARTESIAN_POINT('Ctrl Pts',(9.83762325462799,-2.84862442585767,2.69245362484614));
#5626=CARTESIAN_POINT('Ctrl Pts',(9.84346698885961,-2.84862442585767,2.70859905909217));
#5627=CARTESIAN_POINT('',(9.24126248314343,-2.84862442585767,1.50713517738358));
#5628=CARTESIAN_POINT('',(13.3346225254169,-2.84862442585767,1.50713517738359));
#5629=CARTESIAN_POINT('',(8.77665954841816,-2.84682622407918,2.71029357769836));
#5630=CARTESIAN_POINT('Ctrl Pts',(8.77679361475528,-2.84862442585767,2.70860756651644));
#5631=CARTESIAN_POINT('Ctrl Pts',(8.78379792777184,-2.84862442585767,2.69251369706502));
#5632=CARTESIAN_POINT('Ctrl Pts',(8.79078230243175,-2.84862442585767,2.67640964375849));
#5633=CARTESIAN_POINT('Ctrl Pts',(8.8753576224118,-2.84862442585767,2.48069807460854));
#5634=CARTESIAN_POINT('Ctrl Pts',(8.95123295617157,-2.8486244273253,2.29789414186475));
#5635=CARTESIAN_POINT('Ctrl Pts',(9.10046525102538,-2.8486244273253,1.91583271764201));
#5636=CARTESIAN_POINT('Ctrl Pts',(9.17497777181831,-2.84862442585767,1.71136117817557));
#5637=CARTESIAN_POINT('Ctrl Pts',(9.24126248314343,-2.84862442585767,1.50713517738359));
#5638=CARTESIAN_POINT('',(8.59333250457579,-2.84682735336114,2.71029427328404));
#5639=CARTESIAN_POINT('',(11.0238490761438,-2.84862442585767,2.71179421793157));
#5640=CARTESIAN_POINT('',(8.23780938168963,-2.84862442585767,1.50713517738359));
#5641=CARTESIAN_POINT('Ctrl Pts',(8.23780938168964,-2.84862442585767,1.5071351773836));
#5642=CARTESIAN_POINT('Ctrl Pts',(8.28185902228173,-2.84862442585767,1.7116025828885));
#5643=CARTESIAN_POINT('Ctrl Pts',(8.33587259560373,-2.84862442791195,1.91525079323359));
#5644=CARTESIAN_POINT('Ctrl Pts',(8.45094825529517,-2.84862442791195,2.29809205765932));
#5645=CARTESIAN_POINT('Ctrl Pts',(8.51180523038482,-2.84862442585767,2.48054376287594));
#5646=CARTESIAN_POINT('Ctrl Pts',(8.58180849741605,-2.84862442585767,2.67630369365445));
#5647=CARTESIAN_POINT('Ctrl Pts',(8.58762237980882,-2.84862442585767,2.69246241698621));
#5648=CARTESIAN_POINT('Ctrl Pts',(8.59346649505355,-2.84862442585767,2.70860909277272));
#5649=CARTESIAN_POINT('',(7.99126248314343,-2.84862442585767,1.50713517738358));
#5650=CARTESIAN_POINT('',(13.3346225254169,-2.84862442585767,1.50713517738359));
#5651=CARTESIAN_POINT('',(7.52665953824353,-2.84683426299416,2.71029850764342));
#5652=CARTESIAN_POINT('Ctrl Pts',(7.52679307496196,-2.84862442585767,2.70861838061488));
#5653=CARTESIAN_POINT('Ctrl Pts',(7.53379789201695,-2.84862442585767,2.6925231903734));
#5654=CARTESIAN_POINT('Ctrl Pts',(7.54078276765018,-2.84862442585767,2.67641781492382));
#5655=CARTESIAN_POINT('Ctrl Pts',(7.62535873067299,-2.84862442585767,2.48070267374547));
#5656=CARTESIAN_POINT('Ctrl Pts',(7.70123402906389,-2.84862442731812,2.29789681034083));
#5657=CARTESIAN_POINT('Ctrl Pts',(7.85046588841197,-2.84862442731812,1.91583267628874));
#5658=CARTESIAN_POINT('Ctrl Pts',(7.92497771912674,-2.84862442585767,1.7113613405205));
#5659=CARTESIAN_POINT('Ctrl Pts',(7.99126248314342,-2.84862442585767,1.5071351773836));
#5660=CARTESIAN_POINT('',(7.34333249310138,-2.84683551217853,2.71029926941601));
#5661=CARTESIAN_POINT('',(11.0238490761438,-2.84862442585767,2.71179421793157));
#5662=CARTESIAN_POINT('',(6.98780938168963,-2.84862442585767,1.50713517738359));
#5663=CARTESIAN_POINT('Ctrl Pts',(6.98780938168963,-2.84862442585767,1.5071351773836));
#5664=CARTESIAN_POINT('Ctrl Pts',(7.0318590477534,-2.84862442585767,1.71160270112162));
#5665=CARTESIAN_POINT('Ctrl Pts',(7.08587194364161,-2.84862442790181,1.91525079631235));
#5666=CARTESIAN_POINT('Ctrl Pts',(7.20094677397292,-2.84862442790181,2.29809467489166));
#5667=CARTESIAN_POINT('Ctrl Pts',(7.26180352074679,-2.84862442585766,2.48054838492829));
#5668=CARTESIAN_POINT('Ctrl Pts',(7.33180711870137,-2.84862442585766,2.67631193139019));
#5669=CARTESIAN_POINT('Ctrl Pts',(7.33762141389105,-2.84862442585767,2.69247201579432));
#5670=CARTESIAN_POINT('Ctrl Pts',(7.34346594671238,-2.84862442585767,2.70862005097966));
#5671=CARTESIAN_POINT('',(6.74126248314343,-2.84862442585767,1.50713517738358));
#5672=CARTESIAN_POINT('',(13.3346225254169,-2.84862442585767,1.50713517738359));
#5673=CARTESIAN_POINT('',(6.27665951841218,-2.8468431775105,2.71030391927814));
#5674=CARTESIAN_POINT('Ctrl Pts',(6.27679247260682,-2.84862442585767,2.70863024324506));
#5675=CARTESIAN_POINT('Ctrl Pts',(6.28379784512061,-2.84862442585767,2.69253359968691));
#5676=CARTESIAN_POINT('Ctrl Pts',(6.29078327281752,-2.84862442585768,2.67642676942568));
#5677=CARTESIAN_POINT('Ctrl Pts',(6.37535994854178,-2.84862442585768,2.48070770856496));
#5678=CARTESIAN_POINT('Ctrl Pts',(6.45123520736229,-2.84862442731026,2.29789973691976));
#5679=CARTESIAN_POINT('Ctrl Pts',(6.60046659256744,-2.84862442731026,1.91583262505285));
#5680=CARTESIAN_POINT('Ctrl Pts',(6.67497765942542,-2.84862442585767,1.71136152446282));
#5681=CARTESIAN_POINT('Ctrl Pts',(6.74126248314343,-2.84862442585767,1.50713517738359));
#5682=CARTESIAN_POINT('',(6.09333247164065,-2.84684456741434,2.71030475812859));
#5683=CARTESIAN_POINT('',(11.0238490761438,-2.84862442585767,2.71179421793157));
#5684=CARTESIAN_POINT('',(5.73780938168963,-2.84862442585767,1.50713517738359));
#5685=CARTESIAN_POINT('Ctrl Pts',(5.73780938168963,-2.84862442585767,1.5071351773836));
#5686=CARTESIAN_POINT('Ctrl Pts',(5.78185907685439,-2.84862442585767,1.71160283620116));
#5687=CARTESIAN_POINT('Ctrl Pts',(5.83587122068751,-2.84862442789063,1.91525079561866));
#5688=CARTESIAN_POINT('Ctrl Pts',(5.9509451358443,-2.84862442789063,2.29809754881907));
#5689=CARTESIAN_POINT('Ctrl Pts',(6.01180162763585,-2.84862442585767,2.48055345043311));
#5690=CARTESIAN_POINT('Ctrl Pts',(6.08180559131495,-2.84862442585767,2.67632096708642));
#5691=CARTESIAN_POINT('Ctrl Pts',(6.08762034133423,-2.84862442585767,2.69248254974333));
#5692=CARTESIAN_POINT('Ctrl Pts',(6.09346533427394,-2.84862442585767,2.70863208133986));
#5693=CARTESIAN_POINT('',(5.49126248314343,-2.84862442585767,1.50713517738358));
#5694=CARTESIAN_POINT('',(13.3346225254169,-2.84862442585767,1.50713517738359));
#5695=CARTESIAN_POINT('',(5.02665948642913,-2.846853123834,2.71030989419903));
#5696=CARTESIAN_POINT('Ctrl Pts',(5.02679179614449,-2.84862442585767,2.70864333135427));
#5697=CARTESIAN_POINT('Ctrl Pts',(5.03379778445795,-2.84862442585767,2.69254507916332));
#5698=CARTESIAN_POINT('Ctrl Pts',(5.04078382417434,-2.84862442585766,2.67643663859843));
#5699=CARTESIAN_POINT('Ctrl Pts',(5.12536129472081,-2.84862442585766,2.48071325160255));
#5700=CARTESIAN_POINT('Ctrl Pts',(5.20123650898541,-2.84862442730161,2.29790296509866));
#5701=CARTESIAN_POINT('Ctrl Pts',(5.35046737523669,-2.84862442730161,1.91583256170217));
#5702=CARTESIAN_POINT('Ctrl Pts',(5.42497759134768,-2.84862442585767,1.7113617342132));
#5703=CARTESIAN_POINT('Ctrl Pts',(5.49126248314342,-2.84862442585767,1.5071351773836));
#5704=CARTESIAN_POINT('',(4.84333243760253,-2.84685468045443,2.71031082368254));
#5705=CARTESIAN_POINT('',(11.0238490761438,-2.84862442585767,2.71179421793157));
#5706=CARTESIAN_POINT('',(4.48780938168963,-2.84862442585767,1.50713517738359));
#5707=CARTESIAN_POINT('Ctrl Pts',(4.48780938168963,-2.84862442585767,1.5071351773836));
#5708=CARTESIAN_POINT('Ctrl Pts',(4.53185911031318,-2.84862442585767,1.71160299150844));
#5709=CARTESIAN_POINT('Ctrl Pts',(4.58587041394647,-2.84862442787828,1.9152507901144));
#5710=CARTESIAN_POINT('Ctrl Pts',(4.70094331303715,-2.84862442787828,2.29810072324551));
#5711=CARTESIAN_POINT('Ctrl Pts',(4.76179951821517,-2.84862442585766,2.48055903410995));
#5712=CARTESIAN_POINT('Ctrl Pts',(4.83180388858748,-2.84862442585766,2.67633093595801));
#5713=CARTESIAN_POINT('Ctrl Pts',(4.83761914279346,-2.84862442585767,2.69249417782208));
#5714=CARTESIAN_POINT('Ctrl Pts',(4.84346464580177,-2.84862442585767,2.70864536656847));
#5715=CARTESIAN_POINT('',(4.24126248314343,-2.84862442585767,1.50713517738358));
#5716=CARTESIAN_POINT('',(13.3346225254169,-2.84862442585767,1.50713517738359));
#5717=CARTESIAN_POINT('',(3.77665943905189,-2.84686429817697,2.71031653458594));
#5718=CARTESIAN_POINT('Ctrl Pts',(3.77679103100252,-2.84862442585767,2.70865786644558));
#5719=CARTESIAN_POINT('Ctrl Pts',(3.78379770666065,-2.84862442585767,2.69255782170753));
#5720=CARTESIAN_POINT('Ctrl Pts',(3.7907844294769,-2.84862442585767,2.6764475867298));
#5721=CARTESIAN_POINT('Ctrl Pts',(3.87536279264918,-2.84862442585767,2.48071939353203));
#5722=CARTESIAN_POINT('Ctrl Pts',(3.95123795638205,-2.84862442729201,2.29790654931287));
#5723=CARTESIAN_POINT('Ctrl Pts',(4.10046825118152,-2.84862442729201,1.91583248336832));
#5724=CARTESIAN_POINT('Ctrl Pts',(4.17497751316149,-2.84862442585767,1.71136197510816));
#5725=CARTESIAN_POINT('Ctrl Pts',(4.24126248314342,-2.84862442585767,1.5071351773836));
#5726=CARTESIAN_POINT('',(3.59371978829928,-2.84790817158154,2.71073122597795));
#5727=CARTESIAN_POINT('',(11.0238490761438,-2.84862442585767,2.71179421793157));
#5728=CARTESIAN_POINT('',(3.23780938168963,-2.84862442585767,1.50713517738359));
#5729=CARTESIAN_POINT('Ctrl Pts',(3.23780938168963,-2.84862442585767,1.50713517738361));
#5730=CARTESIAN_POINT('Ctrl Pts',(3.28186054745108,-2.84862442585767,1.71160966234283));
#5731=CARTESIAN_POINT('Ctrl Pts',(3.33582269739854,-2.84862442724084,1.91524933773065));
#5732=CARTESIAN_POINT('Ctrl Pts',(3.45073483075678,-2.84862442724084,2.2979205346272));
#5733=CARTESIAN_POINT('Ctrl Pts',(3.51144589960124,-2.84862442585768,2.48014616288996));
#5734=CARTESIAN_POINT('Ctrl Pts',(3.58146712224872,-2.84862442585768,2.67616260726964));
#5735=CARTESIAN_POINT('Ctrl Pts',(3.58743530933706,-2.84862442585767,2.69276463740784));
#5736=CARTESIAN_POINT('Ctrl Pts',(3.59343543922426,-2.84862442585767,2.70935393890616));
#5737=CARTESIAN_POINT('',(3.02384907614375,-2.84862442585767,1.50713517738359));
#5738=CARTESIAN_POINT('',(13.3346225254169,-2.84862442585767,1.50713517738359));
#5739=CARTESIAN_POINT('',(3.02384907614375,-2.84819869582995,-2.12547276695727));
#5740=CARTESIAN_POINT('',(3.02384907614375,-2.84862442585767,-1.40404227860195));
#5741=CARTESIAN_POINT('',(3.18488877059788,-2.84862442585766,-1.50713517738361));
#5742=CARTESIAN_POINT('Ctrl Pts',(3.18488877059788,-2.84862442585767,-1.50713517738361));
#5743=CARTESIAN_POINT('Ctrl Pts',(3.16242044753531,-2.84862442585767,-1.61142750896447));
#5744=CARTESIAN_POINT('Ctrl Pts',(3.137405991007,-2.84862442595863,-1.71531300796113));
#5745=CARTESIAN_POINT('Ctrl Pts',(3.0834656597595,-2.84862442595863,-1.92105514468293));
#5746=CARTESIAN_POINT('Ctrl Pts',(3.0544704326137,-2.84862442585767,-2.02327555320667));
#5747=CARTESIAN_POINT('Ctrl Pts',(3.02384907614375,-2.84862442585767,-2.12477398354848));
#5748=CARTESIAN_POINT('',(3.43143566914408,-2.84862442585766,-1.5071351773836));
#5749=CARTESIAN_POINT('',(13.3346225254169,-2.84862442585767,-1.50713517738359));
#5750=CARTESIAN_POINT('',(3.89603869449459,-2.84686019521323,-2.71031410479823));
#5751=CARTESIAN_POINT('Ctrl Pts',(3.89590683973102,-2.84862442585767,-2.70865254916596));
#5752=CARTESIAN_POINT('Ctrl Pts',(3.88889722083,-2.84862442585767,-2.69254581918906));
#5753=CARTESIAN_POINT('Ctrl Pts',(3.88190757115915,-2.84862442585768,-2.67642888977708));
#5754=CARTESIAN_POINT('Ctrl Pts',(3.79732623229834,-2.84862442585768,-2.48069416593426));
#5755=CARTESIAN_POINT('Ctrl Pts',(3.7214509531498,-2.84862442738219,-2.29788126150319));
#5756=CARTESIAN_POINT('Ctrl Pts',(3.57222405172544,-2.84862442738219,-1.91581557178352));
#5757=CARTESIAN_POINT('Ctrl Pts',(3.49771788311829,-2.84862442585767,-1.71135348373173));
#5758=CARTESIAN_POINT('Ctrl Pts',(3.43143566914408,-2.84862442585767,-1.50713517738359));
#5759=CARTESIAN_POINT('',(4.07936573032278,-2.84685854325951,-2.71031312383777));
#5760=CARTESIAN_POINT('',(11.0238490761438,-2.84862442585767,-2.71179421793157));
#5761=CARTESIAN_POINT('',(4.43488877059788,-2.84862442585766,-1.50713517738361));
#5762=CARTESIAN_POINT('Ctrl Pts',(4.43488877059788,-2.84862442585767,-1.50713517738361));
#5763=CARTESIAN_POINT('Ctrl Pts',(4.39082934716643,-2.84862442585767,-1.71164799237998));
#5764=CARTESIAN_POINT('Ctrl Pts',(4.33680421314192,-2.84862442782486,-1.91534068114032));
#5765=CARTESIAN_POINT('Ctrl Pts',(4.22171428517076,-2.84862442782486,-2.29822947317743));
#5766=CARTESIAN_POINT('Ctrl Pts',(4.16085761026589,-2.84862442585767,-2.48068346557449));
#5767=CARTESIAN_POINT('Ctrl Pts',(4.09086679229697,-2.84862442585767,-2.67641287300669));
#5768=CARTESIAN_POINT('Ctrl Pts',(4.08506533437374,-2.84862442585767,-2.69253763418667));
#5769=CARTESIAN_POINT('Ctrl Pts',(4.07923377064371,-2.84862442585767,-2.70865040206242));
#5770=CARTESIAN_POINT('',(4.68143566914408,-2.84862442585766,-1.5071351773836));
#5771=CARTESIAN_POINT('',(13.3346225254169,-2.84862442585767,-1.50713517738359));
#5772=CARTESIAN_POINT('',(5.1460386529845,-2.84684948021485,-2.71030771277531));
#5773=CARTESIAN_POINT('Ctrl Pts',(5.14590610781719,-2.84862442585767,-2.70863855402169));
#5774=CARTESIAN_POINT('Ctrl Pts',(5.13889714963154,-2.84862442585767,-2.69253354823215));
#5775=CARTESIAN_POINT('Ctrl Pts',(5.13190815660042,-2.84862442585766,-2.67641834479668));
#5776=CARTESIAN_POINT('Ctrl Pts',(5.04732767386717,-2.84862442585766,-2.48068824836471));
#5777=CARTESIAN_POINT('Ctrl Pts',(4.97145234642707,-2.8486244273917,-2.29787781119133));
#5778=CARTESIAN_POINT('Ctrl Pts',(4.82222489298551,-2.8486244273917,-1.91581564514287));
#5779=CARTESIAN_POINT('Ctrl Pts',(4.74771780885373,-2.84862442585767,-1.71135325491949));
#5780=CARTESIAN_POINT('Ctrl Pts',(4.68143566914408,-2.84862442585767,-1.50713517738359));
#5781=CARTESIAN_POINT('',(5.32936569108213,-2.84684801042969,-2.71030683048953));
#5782=CARTESIAN_POINT('',(11.0238490761438,-2.84862442585767,-2.71179421793157));
#5783=CARTESIAN_POINT('',(5.68488877059788,-2.84862442585766,-1.50713517738361));
#5784=CARTESIAN_POINT('Ctrl Pts',(5.68488877059787,-2.84862442585767,-1.50713517738361));
#5785=CARTESIAN_POINT('Ctrl Pts',(5.64082938247698,-2.84862442585767,-1.71164782847729));
#5786=CARTESIAN_POINT('Ctrl Pts',(5.58680337295899,-2.84862442783755,-1.91534068797091));
#5787=CARTESIAN_POINT('Ctrl Pts',(5.47171238880716,-2.84862442783755,-2.29822617883969));
#5788=CARTESIAN_POINT('Ctrl Pts',(5.41085541472201,-2.84862442585768,-2.48067767630624));
#5789=CARTESIAN_POINT('Ctrl Pts',(5.34086501982091,-2.84862442585768,-2.67640253517119));
#5790=CARTESIAN_POINT('Ctrl Pts',(5.335064085706,-2.84862442585767,-2.69252557390748));
#5791=CARTESIAN_POINT('Ctrl Pts',(5.32923305188914,-2.84862442585767,-2.70863662146847));
#5792=CARTESIAN_POINT('',(5.93143566914408,-2.84862442585766,-1.5071351773836));
#5793=CARTESIAN_POINT('',(13.3346225254169,-2.84862442585767,-1.50713517738359));
#5794=CARTESIAN_POINT('',(6.39603862562206,-2.8468399185786,-2.7103019473717));
#5795=CARTESIAN_POINT('Ctrl Pts',(6.39590545902977,-2.84862442585767,-2.70862592165797));
#5796=CARTESIAN_POINT('Ctrl Pts',(6.38889709426525,-2.84862442585767,-2.69252246698333));
#5797=CARTESIAN_POINT('Ctrl Pts',(6.381908691017,-2.84862442585767,-2.67640881627049));
#5798=CARTESIAN_POINT('Ctrl Pts',(6.29732897257062,-2.84862442585767,-2.48068289513417));
#5799=CARTESIAN_POINT('Ctrl Pts',(6.22145360243729,-2.8486244274003,-2.29787469612044));
#5800=CARTESIAN_POINT('Ctrl Pts',(6.07222564657022,-2.8486244274003,-1.91581570455012));
#5801=CARTESIAN_POINT('Ctrl Pts',(5.99771774402429,-2.84862442585767,-1.71135305517723));
#5802=CARTESIAN_POINT('Ctrl Pts',(5.93143566914408,-2.84862442585767,-1.50713517738359));
#5803=CARTESIAN_POINT('',(6.57936566550857,-2.84683860176748,-2.71030114855983));
#5804=CARTESIAN_POINT('',(11.0238490761438,-2.84862442585767,-2.71179421793157));
#5805=CARTESIAN_POINT('',(6.93488877059788,-2.84862442585766,-1.50713517738361));
#5806=CARTESIAN_POINT('Ctrl Pts',(6.93488877059789,-2.84862442585767,-1.5071351773836));
#5807=CARTESIAN_POINT('Ctrl Pts',(6.89082941311706,-2.84862442585767,-1.71164768625373));
#5808=CARTESIAN_POINT('Ctrl Pts',(6.83680262185114,-2.84862442784899,-1.91534068961923));
#5809=CARTESIAN_POINT('Ctrl Pts',(6.72171068862222,-2.84862442784899,-2.29822320309697));
#5810=CARTESIAN_POINT('Ctrl Pts',(6.66085344903225,-2.84862442585767,-2.48067243596248));
#5811=CARTESIAN_POINT('Ctrl Pts',(6.59086343368136,-2.84862442585767,-2.67639318603298));
#5812=CARTESIAN_POINT('Ctrl Pts',(6.58506297100052,-2.84862442585767,-2.69251467300301));
#5813=CARTESIAN_POINT('Ctrl Pts',(6.5792324140922,-2.84862442585767,-2.70862417070381));
#5814=CARTESIAN_POINT('',(7.18143566914408,-2.84862442585767,-1.5071351773836));
#5815=CARTESIAN_POINT('',(13.3346225254169,-2.84862442585767,-1.50713517738359));
#5816=CARTESIAN_POINT('',(7.64603860945592,-2.84683132955625,-2.71029671436601));
#5817=CARTESIAN_POINT('Ctrl Pts',(7.64590487996825,-2.84862442585767,-2.70861444779753));
#5818=CARTESIAN_POINT('Ctrl Pts',(7.63889705165458,-2.84862442585767,-2.69251239752542));
#5819=CARTESIAN_POINT('Ctrl Pts',(7.63190918158326,-2.84862442585767,-2.67640015265958));
#5820=CARTESIAN_POINT('Ctrl Pts',(7.54733015001958,-2.84862442585767,-2.48067802259182));
#5821=CARTESIAN_POINT('Ctrl Pts',(7.47145474188106,-2.84862442740813,-2.29787186609686));
#5822=CARTESIAN_POINT('Ctrl Pts',(7.3222263260763,-2.84862442740813,-1.91581575263515));
#5823=CARTESIAN_POINT('Ctrl Pts',(7.2477176870411,-2.84862442585767,-1.7113528796096));
#5824=CARTESIAN_POINT('Ctrl Pts',(7.18143566914408,-2.84862442585767,-1.50713517738359));
#5825=CARTESIAN_POINT('',(7.8293656507619,-2.84683014249272,-2.71029598689785));
#5826=CARTESIAN_POINT('',(11.0238490761438,-2.84862442585767,-2.71179421793157));
#5827=CARTESIAN_POINT('',(8.18488877059788,-2.84862442585766,-1.50713517738361));
#5828=CARTESIAN_POINT('Ctrl Pts',(8.18488877059787,-2.84862442585767,-1.50713517738361));
#5829=CARTESIAN_POINT('Ctrl Pts',(8.14082943988044,-2.84862442585767,-1.71164756202476));
#5830=CARTESIAN_POINT('Ctrl Pts',(8.08680194594983,-2.84862442785935,-1.91534068721287));
#5831=CARTESIAN_POINT('Ctrl Pts',(7.97170915442048,-2.84862442785935,-2.29822049854839));
#5832=CARTESIAN_POINT('Ctrl Pts',(7.910851677616,-2.84862442585767,-2.48066766373789));
#5833=CARTESIAN_POINT('Ctrl Pts',(7.84086200497834,-2.84862442585767,-2.67638467936083));
#5834=CARTESIAN_POINT('Ctrl Pts',(7.83506196928568,-2.84862442585767,-2.69250475952157));
#5835=CARTESIAN_POINT('Ctrl Pts',(7.82923184430401,-2.84862442585767,-2.70861285213785));
#5836=CARTESIAN_POINT('',(8.43143566914408,-2.84862442585767,-1.5071351773836));
#5837=CARTESIAN_POINT('',(13.3346225254169,-2.84862442585767,-1.50713517738359));
#5838=CARTESIAN_POINT('',(8.89603860220502,-2.84682356859058,-2.71029193815233));
#5839=CARTESIAN_POINT('Ctrl Pts',(8.89590435996554,-2.84862442585767,-2.70860396846321));
#5840=CARTESIAN_POINT('Ctrl Pts',(8.88889701939368,-2.84862442585767,-2.69250319699323));
#5841=CARTESIAN_POINT('Ctrl Pts',(8.881909634102,-2.84862442585767,-2.67639223223817));
#5842=CARTESIAN_POINT('Ctrl Pts',(8.79733122354344,-2.84862442585767,-2.48067356350021));
#5843=CARTESIAN_POINT('Ctrl Pts',(8.72145578136366,-2.84862442741529,-2.29786928082383));
#5844=CARTESIAN_POINT('Ctrl Pts',(8.57222694237506,-2.84862442741529,-1.91581579145778));
#5845=CARTESIAN_POINT('Ctrl Pts',(8.49771763664538,-2.84862442585767,-1.71135272433826));
#5846=CARTESIAN_POINT('Ctrl Pts',(8.43143566914408,-2.84862442585767,-1.50713517738359));
#5847=CARTESIAN_POINT('',(9.07936564464315,-2.84682249256182,-2.71029127221896));
#5848=CARTESIAN_POINT('',(11.0238490761438,-2.84862442585767,-2.71179421793157));
#5849=CARTESIAN_POINT('',(9.43488877059788,-2.84862442585766,-1.5071351773836));
#5850=CARTESIAN_POINT('Ctrl Pts',(9.43488877059788,-2.84862442585767,-1.50713517738359));
#5851=CARTESIAN_POINT('Ctrl Pts',(9.39082946339622,-2.84862442585767,-1.71164745287044));
#5852=CARTESIAN_POINT('Ctrl Pts',(9.33680133416077,-2.8486244278688,-1.91534068162397));
#5853=CARTESIAN_POINT('Ctrl Pts',(9.2217077620153,-2.8486244278688,-2.29821802707406));
#5854=CARTESIAN_POINT('Ctrl Pts',(9.16085007199191,-2.84862442585767,-2.48066329456691));
#5855=CARTESIAN_POINT('Ctrl Pts',(9.09086071058218,-2.84862442585767,-2.67637689747843));
#5856=CARTESIAN_POINT('Ctrl Pts',(9.08506106379369,-2.84862442585767,-2.69249569513711));
#5857=CARTESIAN_POINT('Ctrl Pts',(9.07923133219744,-2.84862442585767,-2.70860250681946));
#5858=CARTESIAN_POINT('',(9.68143566914408,-2.84862442585767,-1.5071351773836));
#5859=CARTESIAN_POINT('',(13.3346225254169,-2.84862442585767,-1.50713517738359));
#5860=CARTESIAN_POINT('',(10.1460386020864,-2.8468165186648,-2.71028755728909));
#5861=CARTESIAN_POINT('Ctrl Pts',(10.1459038904249,-2.84862442585767,-2.70859435034995));
#5862=CARTESIAN_POINT('Ctrl Pts',(10.1388969955833,-2.84862442585767,-2.69249474921214));
#5863=CARTESIAN_POINT('Ctrl Pts',(10.1319100533288,-2.84862442585767,-2.67638495598403));
#5864=CARTESIAN_POINT('Ctrl Pts',(10.0473322072149,-2.84862442585767,-2.48066946312399));
#5865=CARTESIAN_POINT('Ctrl Pts',(9.97145673437474,-2.84862442742187,-2.29786690753779));
#5866=CARTESIAN_POINT('Ctrl Pts',(9.82222750426836,-2.84862442742187,-1.91581582264984));
#5867=CARTESIAN_POINT('Ctrl Pts',(9.74771759182774,-2.84862442585767,-1.71135258625323));
#5868=CARTESIAN_POINT('Ctrl Pts',(9.68143566914409,-2.84862442585767,-1.50713517738361));
#5869=CARTESIAN_POINT('',(10.3289257514711,-2.84771184870989,-2.71054614509517));
#5870=CARTESIAN_POINT('',(11.0238490761438,-2.84862442585767,-2.71179421793157));
#5871=CARTESIAN_POINT('',(10.6848887705979,-2.84862442585766,-1.5071351773836));
#5872=CARTESIAN_POINT('Ctrl Pts',(10.6848887705979,-2.84862442585767,-1.50713517738359));
#5873=CARTESIAN_POINT('Ctrl Pts',(10.6408288271577,-2.84862442585767,-1.71165040613047));
#5874=CARTESIAN_POINT('Ctrl Pts',(10.586823565171,-2.84862442755607,-1.9153402145107));
#5875=CARTESIAN_POINT('Ctrl Pts',(10.4718028413942,-2.84862442755607,-2.29814280868909));
#5876=CARTESIAN_POINT('Ctrl Pts',(10.4110099703332,-2.84862442585767,-2.48048848453579));
#5877=CARTESIAN_POINT('Ctrl Pts',(10.3410124389629,-2.84862442585767,-2.67631715615895));
#5878=CARTESIAN_POINT('Ctrl Pts',(10.3351441403831,-2.84862442585767,-2.69263311564845));
#5879=CARTESIAN_POINT('Ctrl Pts',(10.3292450042586,-2.84862442585767,-2.70893678933792));
#5880=CARTESIAN_POINT('',(13.3346225254169,-2.84862442585767,-1.50713517738359));
#5881=CARTESIAN_POINT('Origin',(3.02384907614375,2.84862442585767,2.80808455720391));
#5882=CARTESIAN_POINT('',(10.6511778487968,2.84808967359283,-2.71093915478704));
#5883=CARTESIAN_POINT('',(11.0238490761438,2.84862442585767,-1.77841863815956));
#5884=CARTESIAN_POINT('Ctrl Pts',(10.6517444165533,2.84862442585767,-2.70958663119422));
#5885=CARTESIAN_POINT('Ctrl Pts',(10.7181155081048,2.84862442585767,-2.5572180519126));
#5886=CARTESIAN_POINT('Ctrl Pts',(10.7831857927431,2.84862442636543,-2.40277143381646));
#5887=CARTESIAN_POINT('Ctrl Pts',(10.9075012055968,2.84862442636543,-2.09344139364087));
#5888=CARTESIAN_POINT('Ctrl Pts',(10.9677673094432,2.84862442585767,-1.93595017012862));
#5889=CARTESIAN_POINT('Ctrl Pts',(11.0238490761437,2.84862442585767,-1.77841863815954));
#5890=CARTESIAN_POINT('',(10.4683325073484,2.84681651858225,-2.71028755728349));
#5891=CARTESIAN_POINT('',(11.0238490761438,2.84862442585767,-2.71179421793157));
#5892=CARTESIAN_POINT('',(10.1128093816896,2.84862442585767,-1.50713517738358));
#5893=CARTESIAN_POINT('Ctrl Pts',(10.1128093816896,2.84862442585767,-1.50713517738361));
#5894=CARTESIAN_POINT('Ctrl Pts',(10.1568589896422,2.84862442585767,-1.71160243138402));
#5895=CARTESIAN_POINT('Ctrl Pts',(10.2108734623886,2.84862442792555,-1.91525078325235));
#5896=CARTESIAN_POINT('Ctrl Pts',(10.3259502311565,2.84862442792555,-2.29808853750365));
#5897=CARTESIAN_POINT('Ctrl Pts',(10.3868075072088,2.84862442585767,-2.48053753211887));
#5898=CARTESIAN_POINT('Ctrl Pts',(10.4568103325124,2.84862442585767,-2.6762925996824));
#5899=CARTESIAN_POINT('Ctrl Pts',(10.4626236619148,2.84862442585767,-2.69244949767383));
#5900=CARTESIAN_POINT('Ctrl Pts',(10.4684672177927,2.84862442585767,-2.70859435034994));
#5901=CARTESIAN_POINT('',(9.86626248314343,2.84862442585767,-1.50713517738359));
#5902=CARTESIAN_POINT('',(13.3346225254169,2.84862442585767,-1.50713517738359));
#5903=CARTESIAN_POINT('',(9.40165955050884,2.84682249264362,-2.71029127222451));
#5904=CARTESIAN_POINT('Ctrl Pts',(9.40179386416001,2.84862442585767,-2.70860250681946));
#5905=CARTESIAN_POINT('Ctrl Pts',(9.40879794213361,2.84862442585767,-2.69250925396209));
#5906=CARTESIAN_POINT('Ctrl Pts',(9.41578208317429,2.84862442585767,-2.67640581787988));
#5907=CARTESIAN_POINT('Ctrl Pts',(9.50035710454219,2.84862442585767,-2.48069591960582));
#5908=CARTESIAN_POINT('Ctrl Pts',(9.57623245461227,2.84862442732866,-2.29789289314525));
#5909=CARTESIAN_POINT('Ctrl Pts',(9.72546495433774,2.84862442732866,-1.91583273517924));
#5910=CARTESIAN_POINT('Ctrl Pts',(9.79997779588513,2.84862442585767,-1.71136110402466));
#5911=CARTESIAN_POINT('Ctrl Pts',(9.86626248314343,2.84862442585767,-1.50713517738359));
#5912=CARTESIAN_POINT('',(9.21833250721586,2.84682356850894,-2.71029193814678));
#5913=CARTESIAN_POINT('',(11.0238490761438,2.84862442585767,-2.71179421793157));
#5914=CARTESIAN_POINT('',(8.86280938168963,2.84862442585767,-1.50713517738358));
#5915=CARTESIAN_POINT('Ctrl Pts',(8.86280938168963,2.84862442585767,-1.5071351773836));
#5916=CARTESIAN_POINT('Ctrl Pts',(8.90685901072075,2.84862442585767,-1.71160252922533));
#5917=CARTESIAN_POINT('Ctrl Pts',(8.96087289825601,2.84862442791668,-1.91525079053687));
#5918=CARTESIAN_POINT('Ctrl Pts',(9.07594894433648,2.84862442791668,-2.29809083397137));
#5919=CARTESIAN_POINT('Ctrl Pts',(9.13680602485858,2.84862442585767,-2.48054159879405));
#5920=CARTESIAN_POINT('Ctrl Pts',(9.20680913788998,2.84862442585767,-2.67629983902876));
#5921=CARTESIAN_POINT('Ctrl Pts',(9.21262282775703,2.84862442585767,-2.69245792713028));
#5922=CARTESIAN_POINT('Ctrl Pts',(9.21846674825203,2.84862442585767,-2.70860396846321));
#5923=CARTESIAN_POINT('',(8.61626248314343,2.84862442585767,-1.50713517738359));
#5924=CARTESIAN_POINT('',(13.3346225254169,2.84862442585767,-1.50713517738359));
#5925=CARTESIAN_POINT('',(8.15165954440541,2.84683014257353,-2.71029598690336));
#5926=CARTESIAN_POINT('Ctrl Pts',(8.15179335205343,2.84862442585767,-2.70861285213785));
#5927=CARTESIAN_POINT('Ctrl Pts',(8.15879791114812,2.84862442585767,-2.69251833761412));
#5928=CARTESIAN_POINT('Ctrl Pts',(8.16578253039036,2.84862442585767,-2.67641363857816));
#5929=CARTESIAN_POINT('Ctrl Pts',(8.25035816386072,2.84862442585767,-2.48070032366843));
#5930=CARTESIAN_POINT('Ctrl Pts',(8.32623348041883,2.84862442732179,-2.29789544620645));
#5931=CARTESIAN_POINT('Ctrl Pts',(8.47546556201146,2.84862442732179,-1.91583269807888));
#5932=CARTESIAN_POINT('Ctrl Pts',(8.54997774627531,2.84862442585767,-1.71136125687463));
#5933=CARTESIAN_POINT('Ctrl Pts',(8.61626248314343,2.84862442585767,-1.50713517738358));
#5934=CARTESIAN_POINT('',(7.9683324999494,2.84683132947567,-2.71029671436051));
#5935=CARTESIAN_POINT('',(11.0238490761438,2.84862442585767,-2.71179421793157));
#5936=CARTESIAN_POINT('',(7.61280938168963,2.84862442585767,-1.50713517738358));
#5937=CARTESIAN_POINT('Ctrl Pts',(7.61280938168963,2.84862442585767,-1.5071351773836));
#5938=CARTESIAN_POINT('Ctrl Pts',(7.65685903460308,2.84862442585767,-1.71160264008112));
#5939=CARTESIAN_POINT('Ctrl Pts',(7.71087227780285,2.84862442790699,-1.91525079518883));
#5940=CARTESIAN_POINT('Ctrl Pts',(7.82594753272231,2.84862442790699,-2.29809333657086));
#5941=CARTESIAN_POINT('Ctrl Pts',(7.88680439671883,2.84862442585767,-2.48054602253814));
#5942=CARTESIAN_POINT('Ctrl Pts',(7.9568078251961,2.84862442585767,-2.67630772013523));
#5943=CARTESIAN_POINT('Ctrl Pts',(7.96262190913101,2.84862442585767,-2.69246710814726));
#5944=CARTESIAN_POINT('Ctrl Pts',(7.96846622824932,2.84862442585767,-2.70861444779752));
#5945=CARTESIAN_POINT('',(7.36626248314343,2.84862442585767,-1.50713517738359));
#5946=CARTESIAN_POINT('',(13.3346225254169,2.84862442585767,-1.50713517738359));
#5947=CARTESIAN_POINT('',(6.90165952967598,2.84683860184717,-2.71030114856527));
#5948=CARTESIAN_POINT('Ctrl Pts',(6.90179278226525,2.84862442585767,-2.70862417070381));
#5949=CARTESIAN_POINT('Ctrl Pts',(6.90879787011014,2.84862442585767,-2.69252827167807));
#5950=CARTESIAN_POINT('Ctrl Pts',(6.91578301488098,2.84862442585767,-2.67642218671447));
#5951=CARTESIAN_POINT('Ctrl Pts',(7.00035932483387,2.84862442585767,-2.48070513252597));
#5952=CARTESIAN_POINT('Ctrl Pts',(7.07623460400956,2.84862442731428,-2.29789823886797));
#5953=CARTESIAN_POINT('Ctrl Pts',(7.2254662314708,2.84862442731428,-1.91583265203173));
#5954=CARTESIAN_POINT('Ctrl Pts',(7.29997769023056,2.84862442585767,-1.71136142955089));
#5955=CARTESIAN_POINT('Ctrl Pts',(7.36626248314343,2.84862442585767,-1.50713517738359));
#5956=CARTESIAN_POINT('',(6.71833248376568,2.84683991849914,-2.71030194736627));
#5957=CARTESIAN_POINT('',(11.0238490761438,2.84862442585767,-2.71179421793157));
#5958=CARTESIAN_POINT('',(6.36280938168963,2.84862442585767,-1.50713517738358));
#5959=CARTESIAN_POINT('Ctrl Pts',(6.36280938168963,2.84862442585767,-1.50713517738361));
#5960=CARTESIAN_POINT('Ctrl Pts',(6.40685906180869,2.84862442585767,-1.71160276636274));
#5961=CARTESIAN_POINT('Ctrl Pts',(6.46087159177102,2.84862442789636,-1.91525079649567));
#5962=CARTESIAN_POINT('Ctrl Pts',(6.57594597610578,2.84862442789636,-2.29809607725535));
#5963=CARTESIAN_POINT('Ctrl Pts',(6.63680259900565,2.84862442585767,-2.48055085796017));
#5964=CARTESIAN_POINT('Ctrl Pts',(6.70680637511918,2.84862442585767,-2.67631634173415));
#5965=CARTESIAN_POINT('Ctrl Pts',(6.71262089204982,2.84862442585767,-2.69247715675436));
#5966=CARTESIAN_POINT('Ctrl Pts',(6.7184656491878,2.84862442585767,-2.70862592165798));
#5967=CARTESIAN_POINT('',(6.11626248314343,2.84862442585767,-1.50713517738359));
#5968=CARTESIAN_POINT('',(13.3346225254169,2.84862442585767,-1.50713517738359));
#5969=CARTESIAN_POINT('',(5.65165950412196,2.84684801050811,-2.71030683049491));
#5970=CARTESIAN_POINT('Ctrl Pts',(5.6517921444683,2.84862442585767,-2.70863662146848));
#5971=CARTESIAN_POINT('Ctrl Pts',(5.65879781670129,2.84862442585767,-2.69253919463776));
#5972=CARTESIAN_POINT('Ctrl Pts',(5.66578354227913,2.84862442585766,-2.67643158029353));
#5973=CARTESIAN_POINT('Ctrl Pts',(5.75036060425611,2.84862442585766,-2.48071041137392));
#5974=CARTESIAN_POINT('Ctrl Pts',(5.82623584147821,2.84862442730604,-2.29790131019802));
#5975=CARTESIAN_POINT('Ctrl Pts',(5.97546697324722,2.84862442730604,-1.91583259505172));
#5976=CARTESIAN_POINT('Ctrl Pts',(6.04997762653236,2.84862442585767,-1.71136162580774));
#5977=CARTESIAN_POINT('Ctrl Pts',(6.11626248314343,2.84862442585767,-1.50713517738359));
#5978=CARTESIAN_POINT('',(5.46833245638334,2.84684948013669,-2.71030771276995));
#5979=CARTESIAN_POINT('',(11.0238490761438,2.84862442585767,-2.71179421793157));
#5980=CARTESIAN_POINT('',(5.11280938168963,2.84862442585767,-1.50713517738358));
#5981=CARTESIAN_POINT('Ctrl Pts',(5.11280938168963,2.84862442585767,-1.50713517738362));
#5982=CARTESIAN_POINT('Ctrl Pts',(5.15685909298675,2.84862442585767,-1.7116029110835));
#5983=CARTESIAN_POINT('Ctrl Pts',(5.2108708287094,2.84862442788461,-1.91525079354619));
#5984=CARTESIAN_POINT('Ctrl Pts',(5.3259442495258,2.84862442788461,-2.2980990953389));
#5985=CARTESIAN_POINT('Ctrl Pts',(5.38680060232149,2.84862442585766,-2.48055617216051));
#5986=CARTESIAN_POINT('Ctrl Pts',(5.45680476378349,2.84862442585766,-2.67632582520572));
#5987=CARTESIAN_POINT('Ctrl Pts',(5.46261975920138,2.84862442585767,-2.69248821564317));
#5988=CARTESIAN_POINT('Ctrl Pts',(5.46846500040038,2.84862442585767,-2.70863855402171));
#5989=CARTESIAN_POINT('',(4.86626248314343,2.84862442585767,-1.50713517738359));
#5990=CARTESIAN_POINT('',(13.3346225254169,2.84862442585767,-1.50713517738359));
#5991=CARTESIAN_POINT('',(4.40165946490359,2.84685854333648,-2.71031312384306));
#5992=CARTESIAN_POINT('Ctrl Pts',(4.40179142571374,2.84862442585767,-2.7086504020624));
#5993=CARTESIAN_POINT('Ctrl Pts',(4.40879774794817,2.84862442585767,-2.69255127864938));
#5994=CARTESIAN_POINT('Ctrl Pts',(4.41578411952675,2.84862442585767,-2.67644196595571));
#5995=CARTESIAN_POINT('Ctrl Pts',(4.50036202302706,2.84862442585767,-2.48071624117288));
#5996=CARTESIAN_POINT('Ctrl Pts',(4.5762372128446,2.84862442729694,-2.29790470877537));
#5997=CARTESIAN_POINT('Ctrl Pts',(4.72546780048414,2.84862442729694,-1.91583252461549));
#5998=CARTESIAN_POINT('Ctrl Pts',(4.79997755364427,2.84862442585767,-1.71136185037904));
#5999=CARTESIAN_POINT('Ctrl Pts',(4.86626248314343,2.84862442585767,-1.50713517738359));
#6000=CARTESIAN_POINT('',(4.21833241485052,2.84686019513654,-2.71031410479295));
#6001=CARTESIAN_POINT('',(11.0238490761438,2.84862442585767,-2.71179421793157));
#6002=CARTESIAN_POINT('',(3.86280938168963,2.84862442585767,-1.50713517738358));
#6003=CARTESIAN_POINT('Ctrl Pts',(3.86280938168963,2.84862442585767,-1.50713517738361));
#6004=CARTESIAN_POINT('Ctrl Pts',(3.90685912895696,2.84862442585767,-1.71160307804822));
#6005=CARTESIAN_POINT('Ctrl Pts',(3.9608699742735,2.84862442787157,-1.91525078515163));
#6006=CARTESIAN_POINT('Ctrl Pts',(4.07594232175518,2.84862442787157,-2.29810243978791));
#6007=CARTESIAN_POINT('Ctrl Pts',(4.13679836986563,2.84862442585768,-2.48056204862024));
#6008=CARTESIAN_POINT('Ctrl Pts',(4.20680296129537,2.84862442585768,-2.67633632166697));
#6009=CARTESIAN_POINT('Ctrl Pts',(4.21261848888836,2.84862442585767,-2.69250046252893));
#6010=CARTESIAN_POINT('Ctrl Pts',(4.21846426848655,2.84862442585767,-2.70865254916597));
#6011=CARTESIAN_POINT('',(3.61626248314343,2.84862442585767,-1.50713517738359));
#6012=CARTESIAN_POINT('',(13.3346225254169,2.84862442585767,-1.50713517738359));
#6013=CARTESIAN_POINT('',(3.15165940830577,2.8468704213803,-2.71032014357828));
#6014=CARTESIAN_POINT('Ctrl Pts',(3.15179060954266,2.84862442585767,-2.70866576166606));
#6015=CARTESIAN_POINT('Ctrl Pts',(3.15879766001169,2.84862442585767,-2.69256474069428));
#6016=CARTESIAN_POINT('Ctrl Pts',(3.1657847553136,2.84862442585768,-2.6764535284648));
#6017=CARTESIAN_POINT('Ctrl Pts',(3.25036360752406,2.84862442585768,-2.48072272386991));
#6018=CARTESIAN_POINT('Ctrl Pts',(3.32623874336682,2.84862442728679,-2.29790849584301));
#6019=CARTESIAN_POINT('Ctrl Pts',(3.4754687298166,2.84862442728679,-1.91583243746613));
#6020=CARTESIAN_POINT('Ctrl Pts',(3.54997746960448,2.84862442585767,-1.71136210930917));
#6021=CARTESIAN_POINT('Ctrl Pts',(3.61626248314343,2.84862442585767,-1.50713517738359));
#6022=CARTESIAN_POINT('',(3.02384907614375,2.84862442585767,-2.71179421793157));
#6023=CARTESIAN_POINT('',(11.0238490761438,2.84862442585767,-2.71179421793157));
#6024=CARTESIAN_POINT('',(3.02384907614375,2.84862442585767,2.11350930841789));
#6025=CARTESIAN_POINT('',(3.02384907614375,2.84862442585767,1.40404227860195));
#6026=CARTESIAN_POINT('',(3.27141298814991,2.84845804217612,2.71158690494159));
#6027=CARTESIAN_POINT('Ctrl Pts',(3.27100497985698,2.84862442585767,2.71079938718163));
#6028=CARTESIAN_POINT('Ctrl Pts',(3.228076353399,2.84862442585767,2.61225572759565));
#6029=CARTESIAN_POINT('Ctrl Pts',(3.18578823704266,2.84862442598707,2.51303020389064));
#6030=CARTESIAN_POINT('Ctrl Pts',(3.10334913028736,2.84862442598707,2.31421002248986));
#6031=CARTESIAN_POINT('Ctrl Pts',(3.06291723376633,2.84862442585767,2.21392684695503));
#6032=CARTESIAN_POINT('Ctrl Pts',(3.02384907614376,2.84862442585767,2.11350930841789));
#6033=CARTESIAN_POINT('',(3.45436575618682,2.84686429810077,2.7103165345807));
#6034=CARTESIAN_POINT('',(11.0238490761438,2.84862442585767,2.71179421793157));
#6035=CARTESIAN_POINT('',(3.80988877059788,2.84862442585767,1.5071351773836));
#6036=CARTESIAN_POINT('Ctrl Pts',(3.80988877059788,2.84862442585767,1.5071351773836));
#6037=CARTESIAN_POINT('Ctrl Pts',(3.7658293274531,2.84862442585767,1.71164808388438));
#6038=CARTESIAN_POINT('Ctrl Pts',(3.7118046719511,2.84862442781797,1.9153406753387));
#6039=CARTESIAN_POINT('Ctrl Pts',(3.59671531847852,2.84862442781797,2.29823125790659));
#6040=CARTESIAN_POINT('Ctrl Pts',(3.53585880786088,2.84862442585766,2.48068659685609));
#6041=CARTESIAN_POINT('Ctrl Pts',(3.46586775948282,2.84862442585766,2.67641846844891));
#6042=CARTESIAN_POINT('Ctrl Pts',(3.46006601698536,2.84862442585767,2.69254416467973));
#6043=CARTESIAN_POINT('Ctrl Pts',(3.45423416535493,2.84862442585767,2.7086578664456));
#6044=CARTESIAN_POINT('',(4.05643566914408,2.84862442585766,1.50713517738361));
#6045=CARTESIAN_POINT('',(13.3346225254169,2.84862442585767,1.50713517738359));
#6046=CARTESIAN_POINT('',(4.52103867175434,2.84685468053191,2.71031082368787));
#6047=CARTESIAN_POINT('Ctrl Pts',(4.52090646241579,2.84862442585767,2.70864536656847));
#6048=CARTESIAN_POINT('Ctrl Pts',(4.51389718302579,2.84862442585767,2.69253952221217));
#6049=CARTESIAN_POINT('Ctrl Pts',(4.50690787077022,2.84862442585768,2.67642347934393));
#6050=CARTESIAN_POINT('Ctrl Pts',(4.42232697249459,2.84862442585768,2.48069113060106));
#6051=CARTESIAN_POINT('Ctrl Pts',(4.34645166843461,2.84862442738707,2.29787949083546));
#6052=CARTESIAN_POINT('Ctrl Pts',(4.19722448429369,2.84862442738707,1.91581561039782));
#6053=CARTESIAN_POINT('Ctrl Pts',(4.12271784469148,2.84862442585767,1.7113533653371));
#6054=CARTESIAN_POINT('Ctrl Pts',(4.05643566914409,2.84862442585767,1.50713517738361));
#6055=CARTESIAN_POINT('',(4.70436570878572,2.84685312375625,2.71030989419369));
#6056=CARTESIAN_POINT('',(11.0238490761438,2.84862442585767,2.71179421793157));
#6057=CARTESIAN_POINT('',(5.05988877059788,2.84862442585767,1.5071351773836));
#6058=CARTESIAN_POINT('Ctrl Pts',(5.05988877059787,2.84862442585767,1.50713517738362));
#6059=CARTESIAN_POINT('Ctrl Pts',(5.01582936546295,2.84862442585767,1.71164790745213));
#6060=CARTESIAN_POINT('Ctrl Pts',(4.96180378091768,2.84862442783138,1.91534068528627));
#6061=CARTESIAN_POINT('Ctrl Pts',(4.84671331029461,2.84862442783138,2.29822778278234));
#6062=CARTESIAN_POINT('Ctrl Pts',(4.78585648120188,2.84862442585767,2.48068049652974));
#6063=CARTESIAN_POINT('Ctrl Pts',(4.71586588068668,2.84862442585767,2.6764075700122));
#6064=CARTESIAN_POINT('Ctrl Pts',(4.71006469178374,2.84862442585767,2.69253144678897));
#6065=CARTESIAN_POINT('Ctrl Pts',(4.70423340021296,2.84862442585767,2.70864333135427));
#6066=CARTESIAN_POINT('',(5.30643566914408,2.84862442585766,1.50713517738361));
#6067=CARTESIAN_POINT('',(13.3346225254169,2.84862442585767,1.50713517738359));
#6068=CARTESIAN_POINT('',(5.77103863773745,2.8468445674932,2.71030475813399));
#6069=CARTESIAN_POINT('Ctrl Pts',(5.77090577394363,2.84862442585767,2.70863208133986));
#6070=CARTESIAN_POINT('Ctrl Pts',(5.7638971201788,2.84862442585767,2.69252787095137));
#6071=CARTESIAN_POINT('Ctrl Pts',(5.75690842970124,2.84862442585768,2.67641346374591));
#6072=CARTESIAN_POINT('Ctrl Pts',(5.67232833961162,2.84862442585768,2.48068550687512));
#6073=CARTESIAN_POINT('Ctrl Pts',(5.59645299018697,2.84862442739611,2.29787621515313));
#6074=CARTESIAN_POINT('Ctrl Pts',(5.44722527981436,2.84862442739611,1.91581567641076));
#6075=CARTESIAN_POINT('Ctrl Pts',(5.3727177753678,2.84862442585767,1.71135315174791));
#6076=CARTESIAN_POINT('Ctrl Pts',(5.30643566914408,2.84862442585767,1.5071351773836));
#6077=CARTESIAN_POINT('',(5.95436567678183,2.84684317743142,2.71030391927272));
#6078=CARTESIAN_POINT('',(11.0238490761438,2.84862442585767,2.71179421793157));
#6079=CARTESIAN_POINT('',(6.30988877059788,2.84862442585767,1.5071351773836));
#6080=CARTESIAN_POINT('Ctrl Pts',(6.30988877059789,2.84862442585767,1.5071351773836));
#6081=CARTESIAN_POINT('Ctrl Pts',(6.2658293983268,2.84862442585767,1.71164775490643));
#6082=CARTESIAN_POINT('Ctrl Pts',(6.21180298721187,2.84862442784341,1.91534068936543));
#6083=CARTESIAN_POINT('Ctrl Pts',(6.09671151624063,2.84862442784341,2.29822465435504));
#6084=CARTESIAN_POINT('Ctrl Pts',(6.03585440555947,2.84862442585767,2.48067499299047));
#6085=CARTESIAN_POINT('Ctrl Pts',(5.96586420541966,2.84862442585767,2.67639774691987));
#6086=CARTESIAN_POINT('Ctrl Pts',(5.96006351303068,2.84862442585767,2.69251999018277));
#6087=CARTESIAN_POINT('Ctrl Pts',(5.95423272375062,2.84862442585767,2.70863024324505));
#6088=CARTESIAN_POINT('',(6.55643566914408,2.84862442585766,1.50713517738361));
#6089=CARTESIAN_POINT('',(13.3346225254169,2.84862442585767,1.50713517738359));
#6090=CARTESIAN_POINT('',(7.02103861629541,2.84683551225861,2.71029926942148));
#6091=CARTESIAN_POINT('Ctrl Pts',(7.02090516150519,2.84862442585767,2.70862005097967));
#6092=CARTESIAN_POINT('Ctrl Pts',(7.01389707152942,2.84862442585767,2.69251731541987));
#6093=CARTESIAN_POINT('Ctrl Pts',(7.0069089413909,2.84862442585767,2.67640438456248));
#6094=CARTESIAN_POINT('Ctrl Pts',(6.92232957528187,2.84862442585767,2.48068040331129));
#6095=CARTESIAN_POINT('Ctrl Pts',(6.84645418560907,2.84862442740432,2.29787324819636));
#6096=CARTESIAN_POINT('Ctrl Pts',(6.6972259948484,2.84862442740432,1.91581572986742));
#6097=CARTESIAN_POINT('Ctrl Pts',(6.62271771463721,2.84862442585767,1.71135296463439));
#6098=CARTESIAN_POINT('Ctrl Pts',(6.55643566914408,2.84862442585767,1.5071351773836));
#6099=CARTESIAN_POINT('',(7.20436565693214,2.84683426291388,2.71029850763795));
#6100=CARTESIAN_POINT('',(11.0238490761438,2.84862442585767,2.71179421793157));
#6101=CARTESIAN_POINT('',(7.55988877059788,2.84862442585767,1.5071351773836));
#6102=CARTESIAN_POINT('Ctrl Pts',(7.55988877059788,2.84862442585767,1.5071351773836));
#6103=CARTESIAN_POINT('Ctrl Pts',(7.51582942694069,2.84862442585767,1.71164762208787));
#6104=CARTESIAN_POINT('Ctrl Pts',(7.46180227524923,2.84862442785429,1.91534068886327));
#6105=CARTESIAN_POINT('Ctrl Pts',(7.34670990240678,2.84862442785429,2.29822181949426));
#6106=CARTESIAN_POINT('Ctrl Pts',(7.28585254096374,2.84862442585767,2.48066999572136));
#6107=CARTESIAN_POINT('Ctrl Pts',(7.2158627012126,2.84862442585767,2.67638883532302));
#6108=CARTESIAN_POINT('Ctrl Pts',(7.21006245715211,2.84862442585767,2.69250960216246));
#6109=CARTESIAN_POINT('Ctrl Pts',(7.20423212139549,2.84862442585767,2.70861838061489));
#6110=CARTESIAN_POINT('',(7.80643566914408,2.84862442585766,1.50713517738361));
#6111=CARTESIAN_POINT('',(13.3346225254169,2.84862442585767,1.50713517738359));
#6112=CARTESIAN_POINT('',(8.27103860483754,2.84682735344229,2.71029427328957));
#6113=CARTESIAN_POINT('Ctrl Pts',(8.27090461316402,2.84862442585767,2.70860909277273));
#6114=CARTESIAN_POINT('Ctrl Pts',(8.26389703435909,2.84862442585767,2.69250769644918));
#6115=CARTESIAN_POINT('Ctrl Pts',(8.25690941227972,2.84862442585767,2.67639610620256));
#6116=CARTESIAN_POINT('Ctrl Pts',(8.17233069882605,2.84862442585767,2.48067574504101));
#6117=CARTESIAN_POINT('Ctrl Pts',(8.0964552732107,2.84862442741179,2.29787054506796));
#6118=CARTESIAN_POINT('Ctrl Pts',(7.94722664153419,2.84862442741179,1.91581577309339));
#6119=CARTESIAN_POINT('Ctrl Pts',(7.87271766108794,2.84862442585767,1.71135279964682));
#6120=CARTESIAN_POINT('Ctrl Pts',(7.80643566914409,2.84862442585767,1.50713517738362));
#6121=CARTESIAN_POINT('',(8.45436564674126,2.84682622399784,2.71029357769283));
#6122=CARTESIAN_POINT('',(11.0238490761438,2.84862442585767,2.71179421793157));
#6123=CARTESIAN_POINT('',(8.80988877059788,2.84862442585767,1.50713517738359));
#6124=CARTESIAN_POINT('Ctrl Pts',(8.80988877059788,2.84862442585767,1.50713517738359));
#6125=CARTESIAN_POINT('Ctrl Pts',(8.76582945201024,2.84862442585767,1.7116475057213));
#6126=CARTESIAN_POINT('Ctrl Pts',(8.71180163264592,2.84862442786418,1.91534068476964));
#6127=CARTESIAN_POINT('Ctrl Pts',(8.59670844181264,2.84862442786418,2.29821923576154));
#6128=CARTESIAN_POINT('Ctrl Pts',(8.53585085563285,2.84862442585767,2.48066543233191));
#6129=CARTESIAN_POINT('Ctrl Pts',(8.46586134225275,2.84862442585767,2.67638070425965));
#6130=CARTESIAN_POINT('Ctrl Pts',(8.46006150542514,2.84862442585767,2.69250012875935));
#6131=CARTESIAN_POINT('Ctrl Pts',(8.45423158160217,2.84862442585767,2.70860756651644));
#6132=CARTESIAN_POINT('',(9.05643566914408,2.84862442585766,1.50713517738361));
#6133=CARTESIAN_POINT('',(13.3346225254169,2.84862442585767,1.50713517738359));
#6134=CARTESIAN_POINT('',(9.52103860134977,2.8468199611698,2.71028970168337));
#6135=CARTESIAN_POINT('Ctrl Pts',(9.52090411935796,2.84862442585767,2.70859905909218));
#6136=CARTESIAN_POINT('Ctrl Pts',(9.51389700653417,2.84862442585767,2.69249888540408));
#6137=CARTESIAN_POINT('Ctrl Pts',(9.50690984761346,2.84862442585768,2.67638851904301));
#6138=CARTESIAN_POINT('Ctrl Pts',(9.42233172583661,2.84862442585768,2.48067147148852));
#6139=CARTESIAN_POINT('Ctrl Pts',(9.3464562679359,2.84862442741865,2.29786806948615));
#6140=CARTESIAN_POINT('Ctrl Pts',(9.19722722963917,2.84862442741865,1.9158158079193));
#6141=CARTESIAN_POINT('Ctrl Pts',(9.12271761359435,2.84862442585767,1.71135265331708));
#6142=CARTESIAN_POINT('Ctrl Pts',(9.05643566914409,2.84862442585767,1.50713517738362));
#6143=CARTESIAN_POINT('',(9.70436564426604,2.84681893475664,2.71028906341284));
#6144=CARTESIAN_POINT('',(11.0238490761438,2.84862442585767,2.71179421793157));
#6145=CARTESIAN_POINT('',(10.0598887705979,2.84862442585767,1.50713517738359));
#6146=CARTESIAN_POINT('Ctrl Pts',(10.0598887705979,2.84862442585767,1.50713517738359));
#6147=CARTESIAN_POINT('Ctrl Pts',(10.0158294740978,2.84862442585767,1.71164740319615));
#6148=CARTESIAN_POINT('Ctrl Pts',(9.96180104943227,2.84862442787322,1.91534067785543));
#6149=CARTESIAN_POINT('Ctrl Pts',(9.84670711270893,2.84862442787322,2.29821686881042));
#6150=CARTESIAN_POINT('Ctrl Pts',(9.78584932396424,2.84862442585767,2.48066124415883));
#6151=CARTESIAN_POINT('Ctrl Pts',(9.71586010775059,2.84862442585767,2.67637324766241));
#6152=CARTESIAN_POINT('Ctrl Pts',(9.71006064278651,2.84862442585767,2.69249144531452));
#6153=CARTESIAN_POINT('Ctrl Pts',(9.70423109510515,2.84862442585767,2.70859765771964));
#6154=CARTESIAN_POINT('',(10.3064356691441,2.84862442585766,1.50713517738361));
#6155=CARTESIAN_POINT('',(13.3346225254169,2.84862442585767,1.50713517738359));
#6156=CARTESIAN_POINT('',(10.7710386042496,2.84681322972354,2.71028549897447));
#6157=CARTESIAN_POINT('Ctrl Pts',(10.7709036723368,2.84862442585767,2.70858982922371));
#6158=CARTESIAN_POINT('Ctrl Pts',(10.7638969863635,2.84862442585767,2.69249077707409));
#6159=CARTESIAN_POINT('Ctrl Pts',(10.7569102517173,2.84862442585767,2.67638153338721));
#6160=CARTESIAN_POINT('Ctrl Pts',(10.6723326690498,2.84862442585767,2.48066753305333));
#6161=CARTESIAN_POINT('Ctrl Pts',(10.5964571819956,2.84862442742496,2.29786579177956));
#6162=CARTESIAN_POINT('Ctrl Pts',(10.4472277671172,2.84862442742496,1.91581583580293));
#6163=CARTESIAN_POINT('Ctrl Pts',(10.3727175712488,2.84862442585767,1.71135252284851));
#6164=CARTESIAN_POINT('Ctrl Pts',(10.3064356691441,2.84862442585767,1.5071351773836));
#6165=CARTESIAN_POINT('',(10.9543681768003,2.84860418144656,2.71177492056083));
#6166=CARTESIAN_POINT('',(11.0238490761438,2.84862442585767,2.71179421793157));
#6167=CARTESIAN_POINT('',(11.0238490761438,2.84862442585767,2.5145657703754));
#6168=CARTESIAN_POINT('Ctrl Pts',(11.0238490761438,2.84862442585767,2.51456577037539));
#6169=CARTESIAN_POINT('Ctrl Pts',(11.0125388019847,2.84862442585767,2.54755700411209));
#6170=CARTESIAN_POINT('Ctrl Pts',(11.0010794330984,2.84862442585774,2.58050639119045));
#6171=CARTESIAN_POINT('Ctrl Pts',(10.9781080325486,2.84862442585774,2.6456791051022));
#6172=CARTESIAN_POINT('Ctrl Pts',(10.9665953160741,2.84862442585767,2.67792052124666));
#6173=CARTESIAN_POINT('Ctrl Pts',(10.9547630945647,2.84862442585767,2.71065726237697));
#6174=CARTESIAN_POINT('Ctrl Pts',(10.9545649113151,2.84862442585767,2.71120547217373));
#6175=CARTESIAN_POINT('Ctrl Pts',(10.9543666920789,2.84862442585767,2.71175366890678));
#6176=CARTESIAN_POINT('',(11.0238490761438,2.84862442585767,-6.75363122348402));
#6177=CARTESIAN_POINT('Origin',(13.3346225254169,0.,0.));
#6178=CARTESIAN_POINT('',(3.02409152551386,-0.0272219868854266,3.22221592290483));
#6179=CARTESIAN_POINT('Ctrl Pts',(3.23780938168962,-2.84862442585767,1.50713517738359));
#6180=CARTESIAN_POINT('Ctrl Pts',(3.22442453716735,-2.74722502408512,1.69878939459725));
#6181=CARTESIAN_POINT('Ctrl Pts',(3.21148030385348,-2.62674430926649,1.87972173710279));
#6182=CARTESIAN_POINT('Ctrl Pts',(3.18515854827395,-2.35116852031272,2.21476896718337));
#6183=CARTESIAN_POINT('Ctrl Pts',(3.17183872397072,-2.19678014965427,2.36798232659674));
#6184=CARTESIAN_POINT('Ctrl Pts',(3.1491421401168,-1.91598526745743,2.59537315704631));
#6185=CARTESIAN_POINT('Ctrl Pts',(3.13997414564689,-1.79781120104803,2.6785880739654));
#6186=CARTESIAN_POINT('Ctrl Pts',(3.11246007094934,-1.42767513520865,2.90366763005427));
#6187=CARTESIAN_POINT('Ctrl Pts',(3.09467202235144,-1.16180919607831,3.01989665639061));
#6188=CARTESIAN_POINT('Ctrl Pts',(3.05986689150469,-0.605250308275812,3.17864929438211));
#6189=CARTESIAN_POINT('Ctrl Pts',(3.04244620156952,-0.317070870595313,3.22018452284352));
#6190=CARTESIAN_POINT('Ctrl Pts',(3.0243364807485,-0.0272455238111505,3.22263482944194));
#6191=CARTESIAN_POINT('Origin',(3.02384907614375,0.,0.));
#6192=CARTESIAN_POINT('Origin',(13.3346225254169,0.,0.));
#6193=CARTESIAN_POINT('Ctrl Pts',(3.61626248314344,2.84862442585767,-1.50713517738358));
#6194=CARTESIAN_POINT('Ctrl Pts',(3.59307108387217,2.67293362807053,-1.83920698188073));
#6195=CARTESIAN_POINT('Ctrl Pts',(3.56888016255196,2.44052702935851,-2.13802203875356));
#6196=CARTESIAN_POINT('Ctrl Pts',(3.52292662769557,1.88507649015484,-2.64043283240736));
#6197=CARTESIAN_POINT('Ctrl Pts',(3.50145575366532,1.56693992247333,-2.84078534752095));
#6198=CARTESIAN_POINT('Ctrl Pts',(3.45301242989295,0.83394564202971,-3.14104684531098));
#6199=CARTESIAN_POINT('Ctrl Pts',(3.42556936284725,0.419015787858895,-3.22274339729798));
#6200=CARTESIAN_POINT('Ctrl Pts',(3.37393448273109,-0.418922408506109,-3.22275660206917));
#6201=CARTESIAN_POINT('Ctrl Pts',(3.35014729256515,-0.833858370849191,-3.14106853204561));
#6202=CARTESIAN_POINT('Ctrl Pts',(3.30059617351017,-1.56685554891026,-2.84083243276982));
#6203=CARTESIAN_POINT('Ctrl Pts',(3.27632232182658,-1.8850119004154,-2.6404833146547));
#6204=CARTESIAN_POINT('Ctrl Pts',(3.22990333374809,-2.44049642846581,-2.13805771006364));
#6205=CARTESIAN_POINT('Ctrl Pts',(3.20808192590441,-2.67292032489589,-1.83923212610718));
#6206=CARTESIAN_POINT('Ctrl Pts',(3.18488877059789,-2.84862442585765,-1.50713517738362));
#6207=CARTESIAN_POINT('Ctrl Pts',(3.86280938168963,2.84862442585767,-1.50713517738358));
#6208=CARTESIAN_POINT('Ctrl Pts',(3.83961637099924,2.67292142046256,-1.83923005538518));
#6209=CARTESIAN_POINT('Ctrl Pts',(3.81779859998544,2.4404992595268,-2.13805411438247));
#6210=CARTESIAN_POINT('Ctrl Pts',(3.77138581521096,1.88501876089811,-2.6404781375374));
#6211=CARTESIAN_POINT('Ctrl Pts',(3.74711428478802,1.56686481641917,-2.84082703445761));
#6212=CARTESIAN_POINT('Ctrl Pts',(3.69756239352038,0.833866711494175,-3.14106691461616));
#6213=CARTESIAN_POINT('Ctrl Pts',(3.67377245274625,0.418926363378426,-3.22275665847088));
#6214=CARTESIAN_POINT('Ctrl Pts',(3.62213600150572,-0.419020559361353,-3.2227433408852));
#6215=CARTESIAN_POINT('Ctrl Pts',(3.59469416940512,-0.833954782426799,-3.14104502062188));
#6216=CARTESIAN_POINT('Ctrl Pts',(3.5462514514891,-1.56694997159161,-2.84077952129024));
#6217=CARTESIAN_POINT('Ctrl Pts',(3.5247792040526,-1.88508393374335,-2.64042719604862));
#6218=CARTESIAN_POINT('Ctrl Pts',(3.47882096430004,-2.44052993660295,-2.13801830515755));
#6219=CARTESIAN_POINT('Ctrl Pts',(3.45462692413533,-2.67293472109094,-1.83920491597139));
#6220=CARTESIAN_POINT('Ctrl Pts',(3.43143566914409,-2.84862442585767,-1.5071351773836));
#6221=CARTESIAN_POINT('Origin',(13.3346225254169,0.,0.));
#6222=CARTESIAN_POINT('Ctrl Pts',(4.48780938168963,-2.84862442585767,1.50713517738358));
#6223=CARTESIAN_POINT('Ctrl Pts',(4.46461645011834,-2.6729220198441,1.83922892249882));
#6224=CARTESIAN_POINT('Ctrl Pts',(4.44280064601111,-2.44050080835351,2.13805214696681));
#6225=CARTESIAN_POINT('Ctrl Pts',(4.39639124959945,-1.88502246104519,2.64047535351999));
#6226=CARTESIAN_POINT('Ctrl Pts',(4.37212100669442,-1.56686976109429,2.84082416041238));
#6227=CARTESIAN_POINT('Ctrl Pts',(4.32256878074722,-0.833871112828827,3.14106606462272));
#6228=CARTESIAN_POINT('Ctrl Pts',(4.29877739278441,-0.418928424370983,3.22275669480111));
#6229=CARTESIAN_POINT('Ctrl Pts',(4.24714010625329,0.419023153943,3.22274330454761));
#6230=CARTESIAN_POINT('Ctrl Pts',(4.21969891604846,0.833959705309191,3.14104403448372));
#6231=CARTESIAN_POINT('Ctrl Pts',(4.17125644341379,1.56695540238117,2.84077637878877));
#6232=CARTESIAN_POINT('Ctrl Pts',(4.14978340883144,1.88508799604372,2.64042412833943));
#6233=CARTESIAN_POINT('Ctrl Pts',(4.10382257494227,2.44053154431161,2.13801624010711));
#6234=CARTESIAN_POINT('Ctrl Pts',(4.07962684434337,2.67293532556987,1.83920377345047));
#6235=CARTESIAN_POINT('Ctrl Pts',(4.05643566914409,2.84862442585766,1.5071351773836));
#6236=CARTESIAN_POINT('Ctrl Pts',(4.24126248314343,-2.84862442585767,1.50713517738358));
#6237=CARTESIAN_POINT('Ctrl Pts',(4.21807117017573,-2.6729342818794,1.83920574612168));
#6238=CARTESIAN_POINT('Ctrl Pts',(4.19387838424026,-2.44052876832755,2.13801980560761));
#6239=CARTESIAN_POINT('Ctrl Pts',(4.14792204906491,-1.88508095777294,2.64042944713896));
#6240=CARTESIAN_POINT('Ctrl Pts',(4.12645036612162,-1.56694596905136,2.84078184008319));
#6241=CARTESIAN_POINT('Ctrl Pts',(4.07800742879564,-0.833951160700149,3.14104574166853));
#6242=CARTESIAN_POINT('Ctrl Pts',(4.05056510798455,-0.419018684053894,3.2227433592853));
#6243=CARTESIAN_POINT('Ctrl Pts',(3.99892928355449,0.418924751693643,3.22275664007429));
#6244=CARTESIAN_POINT('Ctrl Pts',(3.97514043617366,0.833863348516512,3.14106756893928));
#6245=CARTESIAN_POINT('Ctrl Pts',(3.92558883146838,1.56686108050826,2.84082920882958));
#6246=CARTESIAN_POINT('Ctrl Pts',(3.90131635909468,1.88501598412944,2.64048023071256));
#6247=CARTESIAN_POINT('Ctrl Pts',(3.85490107229755,2.44049810801134,2.13805557711095));
#6248=CARTESIAN_POINT('Ctrl Pts',(3.8330818401007,2.67292097491792,1.83923089750562));
#6249=CARTESIAN_POINT('Ctrl Pts',(3.80988877059788,2.84862442585767,1.5071351773836));
#6250=CARTESIAN_POINT('Origin',(13.3346225254169,0.,0.));
#6251=CARTESIAN_POINT('Ctrl Pts',(4.86626248314343,2.84862442585767,-1.50713517738359));
#6252=CARTESIAN_POINT('Ctrl Pts',(4.84307125255646,2.6729349059701,-1.83920456653272));
#6253=CARTESIAN_POINT('Ctrl Pts',(4.81887670737099,2.44053042821952,-2.13801767372441));
#6254=CARTESIAN_POINT('Ctrl Pts',(4.77291769607632,1.88508518038666,-2.64042625393169));
#6255=CARTESIAN_POINT('Ctrl Pts',(4.75144521687828,1.56695164272654,-2.84077855370853));
#6256=CARTESIAN_POINT('Ctrl Pts',(4.70300257961491,0.833956318311138,-3.14104470921497));
#6257=CARTESIAN_POINT('Ctrl Pts',(4.67556094159899,0.419021397612177,-3.22274332225382));
#6258=CARTESIAN_POINT('Ctrl Pts',(4.62392423900021,-0.418926923466486,-3.22275667709832));
#6259=CARTESIAN_POINT('Ctrl Pts',(4.60013386197003,-0.833867976385865,-3.14106667450484));
#6260=CARTESIAN_POINT('Ctrl Pts',(4.55058186393659,-1.56686625632318,-2.84082619705477));
#6261=CARTESIAN_POINT('Ctrl Pts',(4.52631071569599,-1.88501983574479,-2.64047732835315));
#6262=CARTESIAN_POINT('Ctrl Pts',(4.47989894120053,-2.4404997087135,-2.13805354399739));
#6263=CARTESIAN_POINT('Ctrl Pts',(4.45808175832889,-2.67292159439562,-1.83922972663566));
#6264=CARTESIAN_POINT('Ctrl Pts',(4.43488877059788,-2.84862442585766,-1.50713517738361));
#6265=CARTESIAN_POINT('Ctrl Pts',(5.11280938168963,2.84862442585767,-1.50713517738359));
#6266=CARTESIAN_POINT('Ctrl Pts',(5.08961652572833,2.67292259264177,-1.83922783985841));
#6267=CARTESIAN_POINT('Ctrl Pts',(5.06780258054985,2.44050228855337,-2.13805026647637));
#6268=CARTESIAN_POINT('Ctrl Pts',(5.02139640928981,1.88502596245473,-2.64047272456218));
#6269=CARTESIAN_POINT('Ctrl Pts',(4.99712740512678,1.56687440390419,-2.8408214660952));
#6270=CARTESIAN_POINT('Ctrl Pts',(4.94757491926147,0.833875219125953,-3.1410652724995));
#6271=CARTESIAN_POINT('Ctrl Pts',(4.92378219113448,0.418930341135908,-3.22275673021487));
#6272=CARTESIAN_POINT('Ctrl Pts',(4.87214412512137,-0.419025593375922,-3.22274326912658));
#6273=CARTESIAN_POINT('Ctrl Pts',(4.84470352387355,-0.833964322246264,-3.1410431087264));
#6274=CARTESIAN_POINT('Ctrl Pts',(4.79626122682024,-1.56696051586174,-2.8407734241006));
#6275=CARTESIAN_POINT('Ctrl Pts',(4.77478741813673,-1.8850918479804,-2.6404212250909));
#6276=CARTESIAN_POINT('Ctrl Pts',(4.72882409875911,-2.44053308298953,-2.13801426347771));
#6277=CARTESIAN_POINT('Ctrl Pts',(4.70462676797604,-2.67293590410493,-1.83920267996586));
#6278=CARTESIAN_POINT('Ctrl Pts',(4.68143566914409,-2.84862442585766,-1.5071351773836));
#6279=CARTESIAN_POINT('Origin',(13.3346225254169,0.,0.));
#6280=CARTESIAN_POINT('Ctrl Pts',(5.73780938168963,-2.84862442585766,1.5071351773836));
#6281=CARTESIAN_POINT('Ctrl Pts',(5.71461659809079,-2.67292314083723,1.83922680371845));
#6282=CARTESIAN_POINT('Ctrl Pts',(5.69280441295107,-2.44050370523866,2.13804846644808));
#6283=CARTESIAN_POINT('Ctrl Pts',(5.64640131646479,-1.88502928166926,2.64047023752963));
#6284=CARTESIAN_POINT('Ctrl Pts',(5.62213350550393,-1.56687877146956,2.84081893550195));
#6285=CARTESIAN_POINT('Ctrl Pts',(5.57258082594982,-0.833879057355483,3.14106453292806));
#6286=CARTESIAN_POINT('Ctrl Pts',(5.54878685458684,-0.418932127052885,3.22275676474664));
#6287=CARTESIAN_POINT('Ctrl Pts',(5.49714805980877,0.419027891231812,3.22274323458767));
#6288=CARTESIAN_POINT('Ctrl Pts',(5.46970799973081,0.833968660424517,3.14104223801657));
#6289=CARTESIAN_POINT('Ctrl Pts',(5.42126581665765,1.5669653395092,2.8407706408043));
#6290=CARTESIAN_POINT('Ctrl Pts',(5.39979124701918,1.88509550674795,2.6404184726215));
#6291=CARTESIAN_POINT('Ctrl Pts',(5.35382554299669,2.44053455767071,2.13801236883365));
#6292=CARTESIAN_POINT('Ctrl Pts',(5.32962669478367,2.67293645858739,1.8392016319429));
#6293=CARTESIAN_POINT('Ctrl Pts',(5.30643566914408,2.84862442585766,1.5071351773836));
#6294=CARTESIAN_POINT('Ctrl Pts',(5.49126248314343,-2.84862442585767,1.50713517738358));
#6295=CARTESIAN_POINT('Ctrl Pts',(5.46807133131819,-2.67293550264439,1.83920343876331));
#6296=CARTESIAN_POINT('Ctrl Pts',(5.44387512300406,-2.44053201516125,2.13801563527266));
#6297=CARTESIAN_POINT('Ctrl Pts',(5.39791355030629,-1.88508917917162,2.64042323590796));
#6298=CARTESIAN_POINT('Ctrl Pts',(5.37644028777467,-1.56695697751933,2.84077546804639));
#6299=CARTESIAN_POINT('Ctrl Pts',(5.32799787444477,-0.833961148602932,3.14104374133487));
#6300=CARTESIAN_POINT('Ctrl Pts',(5.30055686222276,-0.419023945353596,3.22274328616581));
#6301=CARTESIAN_POINT('Ctrl Pts',(5.24891934126886,0.418928940489715,3.22275671317899));
#6302=CARTESIAN_POINT('Ctrl Pts',(5.22512754956627,0.83387228800949,3.14106584212302));
#6303=CARTESIAN_POINT('Ctrl Pts',(5.17557523973541,1.56687110936966,2.84082337758039));
#6304=CARTESIAN_POINT('Ctrl Pts',(5.15130536434743,1.88502347566865,2.64047459134714));
#6305=CARTESIAN_POINT('Ctrl Pts',(5.1048969289169,2.44050123680849,2.13805160284053));
#6306=CARTESIAN_POINT('Ctrl Pts',(5.08308168026985,2.6729221857465,1.83922860892797));
#6307=CARTESIAN_POINT('Ctrl Pts',(5.05988877059787,2.84862442585766,1.5071351773836));
#6308=CARTESIAN_POINT('Origin',(13.3346225254169,0.,0.));
#6309=CARTESIAN_POINT('Ctrl Pts',(6.11626248314343,2.84862442585767,-1.50713517738359));
#6310=CARTESIAN_POINT('Ctrl Pts',(6.09307140673134,2.67293607395078,-1.83920235894155));
#6311=CARTESIAN_POINT('Ctrl Pts',(6.06887362324604,2.44053353460538,-2.138013683282));
#6312=CARTESIAN_POINT('Ctrl Pts',(6.02290959541348,1.8850929728442,-2.64042037816482));
#6313=CARTESIAN_POINT('Ctrl Pts',(6.00143556263095,1.56696200340518,-2.84077256517489));
#6314=CARTESIAN_POINT('Ctrl Pts',(5.9529933060248,0.833965681264298,-3.14104283220532));
#6315=CARTESIAN_POINT('Ctrl Pts',(5.92555286823777,0.41902634209052,-3.22274325098545));
#6316=CARTESIAN_POINT('Ctrl Pts',(5.87391458317757,-0.418930817396119,-3.2227567483521));
#6317=CARTESIAN_POINT('Ctrl Pts',(5.85012148073232,-0.833876312868828,-3.1410650659791));
#6318=CARTESIAN_POINT('Ctrl Pts',(5.8005689312425,-1.56687566870931,-2.84082073292859));
#6319=CARTESIAN_POINT('Ctrl Pts',(5.77630028091622,-1.88502692192012,-2.64047200537797));
#6320=CARTESIAN_POINT('Ctrl Pts',(5.72989502526017,-2.44050269783885,-2.13804974663392));
#6321=CARTESIAN_POINT('Ctrl Pts',(5.70808160563999,-2.67292275111906,-1.83922754032172));
#6322=CARTESIAN_POINT('Ctrl Pts',(5.68488877059789,-2.84862442585766,-1.50713517738361));
#6323=CARTESIAN_POINT('Ctrl Pts',(6.36280938168962,2.84862442585767,-1.50713517738359));
#6324=CARTESIAN_POINT('Ctrl Pts',(6.33961666743984,2.67292366620393,-1.83922581072696));
#6325=CARTESIAN_POINT('Ctrl Pts',(6.31780615152264,2.44050506298458,-2.13804674109713));
#6326=CARTESIAN_POINT('Ctrl Pts',(6.2714059908784,1.88503243339425,-2.64046788075814));
#6327=CARTESIAN_POINT('Ctrl Pts',(6.24713933049822,1.5668828873788,-2.84081655445888));
#6328=CARTESIAN_POINT('Ctrl Pts',(6.19758651601615,0.833882651370035,-3.14106384120585));
#6329=CARTESIAN_POINT('Ctrl Pts',(6.17379138942913,0.418933793946893,-3.22275679842899));
#6330=CARTESIAN_POINT('Ctrl Pts',(6.12215191209933,-0.419030059540087,-3.22274320089827));
#6331=CARTESIAN_POINT('Ctrl Pts',(6.094712349947,-0.8339727439216,-3.14104141762933));
#6332=CARTESIAN_POINT('Ctrl Pts',(6.04627022633677,-1.56696989769217,-2.84076801434325));
#6333=CARTESIAN_POINT('Ctrl Pts',(6.02479490891982,-1.8850989876462,-2.64041585876965));
#6334=CARTESIAN_POINT('Ctrl Pts',(5.97882691409565,-2.44053597286598,-2.13801055040736));
#6335=CARTESIAN_POINT('Ctrl Pts',(5.95462662454257,-2.67293699071203,-1.83920062617829));
#6336=CARTESIAN_POINT('Ctrl Pts',(5.93143566914408,-2.84862442585766,-1.5071351773836));
#6337=CARTESIAN_POINT('Origin',(13.3346225254169,0.,0.));
#6338=CARTESIAN_POINT('Ctrl Pts',(6.98780938168963,-2.84862442585767,1.50713517738359));
#6339=CARTESIAN_POINT('Ctrl Pts',(6.96461673398571,-2.67292417033464,1.83922485787345));
#6340=CARTESIAN_POINT('Ctrl Pts',(6.94280780367345,-2.44050636590057,2.13804508522705));
#6341=CARTESIAN_POINT('Ctrl Pts',(6.89641045018583,-1.88503543074861,2.64046564385251));
#6342=CARTESIAN_POINT('Ctrl Pts',(6.87214490040623,-1.56688677260614,2.8408143103698));
#6343=CARTESIAN_POINT('Ctrl Pts',(6.82259200319984,-0.833886022336899,3.14106319316094));
#6344=CARTESIAN_POINT('Ctrl Pts',(6.79879580149973,-0.418935352303087,3.22275683129305));
#6345=CARTESIAN_POINT('Ctrl Pts',(6.74715568383361,0.419032109002962,3.22274316802727));
#6346=CARTESIAN_POINT('Ctrl Pts',(6.71971658038225,0.833976594138993,3.14104064336343));
#6347=CARTESIAN_POINT('Ctrl Pts',(6.67127446793275,1.56697421210196,2.8407655317672));
#6348=CARTESIAN_POINT('Ctrl Pts',(6.64979841588627,1.88510230433969,2.64041337268491));
#6349=CARTESIAN_POINT('Ctrl Pts',(6.60382821780123,2.44053733263286,2.13800880301029));
#6350=CARTESIAN_POINT('Ctrl Pts',(6.5796265570515,2.67293750200331,1.83919965979063));
#6351=CARTESIAN_POINT('Ctrl Pts',(6.55643566914408,2.84862442585766,1.50713517738361));
#6352=CARTESIAN_POINT('Ctrl Pts',(6.74126248314343,-2.84862442585767,1.50713517738358));
#6353=CARTESIAN_POINT('Ctrl Pts',(6.71807147903754,-2.67293662172001,1.83920132360723));
#6354=CARTESIAN_POINT('Ctrl Pts',(6.69387220109966,-2.44053499142467,2.13801181152265));
#6355=CARTESIAN_POINT('Ctrl Pts',(6.64790581684408,-1.88509657801398,2.64041766749011));
#6356=CARTESIAN_POINT('Ctrl Pts',(6.62643102697238,-1.56696674689992,2.84076982924885));
#6357=CARTESIAN_POINT('Ctrl Pts',(6.57798886766466,-0.83396994252103,3.14104197668097));
#6358=CARTESIAN_POINT('Ctrl Pts',(6.55054895791701,-0.419028600918373,3.22274321667877));
#6359=CARTESIAN_POINT('Ctrl Pts',(6.49890995808951,0.418932567083949,3.22275678265165));
#6360=CARTESIAN_POINT('Ctrl Pts',(6.47511563910009,0.83388007696913,3.14106434094526));
#6361=CARTESIAN_POINT('Ctrl Pts',(6.42556291388709,1.56687996002487,2.84081824766148));
#6362=CARTESIAN_POINT('Ctrl Pts',(6.40129544396981,1.88503019047376,2.64046955776594));
#6363=CARTESIAN_POINT('Ctrl Pts',(6.35489322120279,2.440504096751,2.13804796912395));
#6364=CARTESIAN_POINT('Ctrl Pts',(6.3330815341862,2.67292329243067,1.83922651719288));
#6365=CARTESIAN_POINT('Ctrl Pts',(6.30988877059789,2.84862442585766,1.5071351773836));
#6366=CARTESIAN_POINT('Origin',(13.3346225254169,0.,0.));
#6367=CARTESIAN_POINT('Ctrl Pts',(7.36626248314343,2.84862442585767,-1.50713517738359));
#6368=CARTESIAN_POINT('Ctrl Pts',(7.34307154845362,2.67293714759447,-1.83920032965602));
#6369=CARTESIAN_POINT('Ctrl Pts',(7.31887085033888,2.44053638999056,-2.13801001440507));
#6370=CARTESIAN_POINT('Ctrl Pts',(7.27290220158661,1.88510000947698,-2.6404150921263));
#6371=CARTESIAN_POINT('Ctrl Pts',(7.25142666779954,1.56697123154665,-2.840767246207));
#6372=CARTESIAN_POINT('Ctrl Pts',(7.20298455318012,0.833973955625731,-3.14104117019823));
#6373=CARTESIAN_POINT('Ctrl Pts',(7.17554512945744,0.419030733458136,-3.22274318321347));
#6374=CARTESIAN_POINT('Ctrl Pts',(7.1239054598541,-0.41893420096316,-3.22275681610992));
#6375=CARTESIAN_POINT('Ctrl Pts',(7.1001100099163,-0.833883603332628,-3.14106366248313));
#6376=CARTESIAN_POINT('Ctrl Pts',(7.05055716572934,-1.56688400609692,-2.84081590809281));
#6377=CARTESIAN_POINT('Ctrl Pts',(7.02629083440148,-1.88503329554496,-2.64046723723885));
#6378=CARTESIAN_POINT('Ctrl Pts',(6.97989150871425,-2.44050543797639,-2.1380462647074));
#6379=CARTESIAN_POINT('Ctrl Pts',(6.95808146568176,-2.67292381139898,-1.83922553629492));
#6380=CARTESIAN_POINT('Ctrl Pts',(6.93488877059789,-2.84862442585766,-1.50713517738361));
#6381=CARTESIAN_POINT('Ctrl Pts',(7.61280938168963,2.84862442585767,-1.50713517738358));
#6382=CARTESIAN_POINT('Ctrl Pts',(7.58961679791791,2.67292465466507,-1.83922394244429));
#6383=CARTESIAN_POINT('Ctrl Pts',(7.56780937603312,2.4405076176909,-2.13804349415313));
#6384=CARTESIAN_POINT('Ctrl Pts',(7.52141471022063,1.88503828547658,-2.64046351751637));
#6385=CARTESIAN_POINT('Ctrl Pts',(7.49715023346056,1.5668904458648,-2.84081219200252));
#6386=CARTESIAN_POINT('Ctrl Pts',(7.44759729996001,0.83388918910371,-3.14106258507959));
#6387=CARTESIAN_POINT('Ctrl Pts',(7.42380009623393,0.418936811450608,-3.2227568633683));
#6388=CARTESIAN_POINT('Ctrl Pts',(7.37215937688665,-0.419034049172175,-3.22274313594519));
#6389=CARTESIAN_POINT('Ctrl Pts',(7.34472069647923,-0.833980230161243,-3.14103991147119));
#6390=CARTESIAN_POINT('Ctrl Pts',(7.29627855235602,-1.56697830211052,-2.84076318151702));
#6391=CARTESIAN_POINT('Ctrl Pts',(7.27480177875458,-1.88510546907338,-2.64041100465428));
#6392=CARTESIAN_POINT('Ctrl Pts',(7.22882945925579,-2.4405386406335,-2.13800712195888));
#6393=CARTESIAN_POINT('Ctrl Pts',(7.20462649212882,-2.67293799383723,-1.83919873017917));
#6394=CARTESIAN_POINT('Ctrl Pts',(7.18143566914407,-2.84862442585766,-1.5071351773836));
#6395=CARTESIAN_POINT('Origin',(13.3346225254169,0.,0.));
#6396=CARTESIAN_POINT('Ctrl Pts',(8.23780938168964,-2.84862442585767,1.50713517738359));
#6397=CARTESIAN_POINT('Ctrl Pts',(8.21461685940783,-2.67292512049342,1.83922306198576));
#6398=CARTESIAN_POINT('Ctrl Pts',(8.19281087455296,-2.44050882170521,2.13804196363864));
#6399=CARTESIAN_POINT('Ctrl Pts',(8.1464187852286,-1.88504100812479,2.64046149341013));
#6400=CARTESIAN_POINT('Ctrl Pts',(8.12215534609299,-1.56689392390231,2.8408101893104));
#6401=CARTESIAN_POINT('Ctrl Pts',(8.07260241763158,-0.833892168503167,3.14106201364612));
#6402=CARTESIAN_POINT('Ctrl Pts',(8.04880427870365,-0.418938179713951,3.22275689468293));
#6403=CARTESIAN_POINT('Ctrl Pts',(7.99716299314995,0.419035888601267,3.22274310462381));
#6404=CARTESIAN_POINT('Ctrl Pts',(7.96972470330544,0.833983669061916,3.14103921859861));
#6405=CARTESIAN_POINT('Ctrl Pts',(7.92128248949699,1.56698218507457,2.84076095324196));
#6406=CARTESIAN_POINT('Ctrl Pts',(7.89980500730298,1.88510849285657,2.64040874595429));
#6407=CARTESIAN_POINT('Ctrl Pts',(7.85383064307685,2.44053990018433,2.13800550301122));
#6408=CARTESIAN_POINT('Ctrl Pts',(7.82962642961006,2.67293846745991,1.83919783498865));
#6409=CARTESIAN_POINT('Ctrl Pts',(7.80643566914408,2.84862442585766,1.50713517738361));
#6410=CARTESIAN_POINT('Ctrl Pts',(7.99126248314343,-2.84862442585768,1.50713517738358));
#6411=CARTESIAN_POINT('Ctrl Pts',(7.96807161517476,-2.67293765305305,1.8391993742927));
#6412=CARTESIAN_POINT('Ctrl Pts',(7.94386956540416,-2.44053773423915,2.13800828689579));
#6413=CARTESIAN_POINT('Ctrl Pts',(7.8978987379663,-1.88510328046092,2.64041264157304));
#6414=CARTESIAN_POINT('Ctrl Pts',(7.87642247339536,-1.56697547832239,2.84076480352758));
#6415=CARTESIAN_POINT('Ctrl Pts',(7.82798035683828,-0.833977741266314,3.1410404086955));
#6416=CARTESIAN_POINT('Ctrl Pts',(7.80054138100634,-0.419032750058116,3.22274315055883));
#6417=CARTESIAN_POINT('Ctrl Pts',(7.74890108275571,0.41893572916163,3.22275684875764));
#6418=CARTESIAN_POINT('Ctrl Pts',(7.72510457983489,0.833886912410527,3.14106302656229));
#6419=CARTESIAN_POINT('Ctrl Pts',(7.67555166710805,1.56688782720213,2.84081370204725));
#6420=CARTESIAN_POINT('Ctrl Pts',(7.65128643511704,1.88503624982873,2.6404650337404));
#6421=CARTESIAN_POINT('Ctrl Pts',(7.60488988062576,2.4405067254997,2.1380446283454));
#6422=CARTESIAN_POINT('Ctrl Pts',(7.58308139992277,2.67292430956845,1.83922459470871));
#6423=CARTESIAN_POINT('Ctrl Pts',(7.55988877059788,2.84862442585767,1.5071351773836));
#6424=CARTESIAN_POINT('Origin',(13.3346225254169,0.,0.));
#6425=CARTESIAN_POINT('Ctrl Pts',(8.61626248314342,2.84862442585767,-1.50713517738359));
#6426=CARTESIAN_POINT('Ctrl Pts',(8.59307167937735,2.6729381394319,-1.83919845499182));
#6427=CARTESIAN_POINT('Ctrl Pts',(8.56886834131465,2.4405390277266,-2.13800662444666));
#6428=CARTESIAN_POINT('Ctrl Pts',(8.52289541547226,1.88510640283117,-2.64041030642139));
#6429=CARTESIAN_POINT('Ctrl Pts',(8.5014184331626,1.56697950597947,-2.84076249002305));
#6430=CARTESIAN_POINT('Ctrl Pts',(8.4529762733107,0.833981317909065,-3.14103968854607));
#6431=CARTESIAN_POINT('Ctrl Pts',(8.42553771068221,0.419034659963695,-3.22274311868561));
#6432=CARTESIAN_POINT('Ctrl Pts',(8.37389682146955,-0.418937160698148,-3.22275688062404));
#6433=CARTESIAN_POINT('Ctrl Pts',(8.3500993367416,-0.833890022429059,-3.14106242959182));
#6434=CARTESIAN_POINT('Ctrl Pts',(8.30054640034428,-1.56689144144792,-2.840811618658));
#6435=CARTESIAN_POINT('Ctrl Pts',(8.27628223077126,-1.88503906470035,-2.64046293826904));
#6436=CARTESIAN_POINT('Ctrl Pts',(8.22988833051641,-2.44050796291601,-2.13804305549113));
#6437=CARTESIAN_POINT('Ctrl Pts',(8.20808133672534,-2.67292478833241,-1.83922368980068));
#6438=CARTESIAN_POINT('Ctrl Pts',(8.18488877059787,-2.84862442585766,-1.50713517738361));
#6439=CARTESIAN_POINT('Ctrl Pts',(8.86280938168963,2.84862442585767,-1.50713517738358));
#6440=CARTESIAN_POINT('Ctrl Pts',(8.83961691861088,2.67292556899732,-1.83922221427203));
#6441=CARTESIAN_POINT('Ctrl Pts',(8.81781230459156,2.44050998098217,-2.1380404898397));
#6442=CARTESIAN_POINT('Ctrl Pts',(8.77142268806627,1.88504360819397,-2.64045956402922));
#6443=CARTESIAN_POINT('Ctrl Pts',(8.74716025315798,1.5668972217526,-2.84080829327991));
#6444=CARTESIAN_POINT('Ctrl Pts',(8.69760736655834,0.833894975613833,-3.14106147589125));
#6445=CARTESIAN_POINT('Ctrl Pts',(8.67380835365215,0.418939464544131,-3.22275692526376));
#6446=CARTESIAN_POINT('Ctrl Pts',(8.62216653451732,-0.419037634971519,-3.22274307403636));
#6447=CARTESIAN_POINT('Ctrl Pts',(8.59472860558992,-0.833986926159643,-3.14103856173539));
#6448=CARTESIAN_POINT('Ctrl Pts',(8.54628628834907,-1.56698587659116,-2.84075883764607));
#6449=CARTESIAN_POINT('Ctrl Pts',(8.52480811038229,-1.88511138561726,-2.64040658872676));
#6450=CARTESIAN_POINT('Ctrl Pts',(8.47883177342321,-2.44054111429785,-2.13800394231365));
#6451=CARTESIAN_POINT('Ctrl Pts',(8.45462636934577,-2.67293892400329,-1.83919697207958));
#6452=CARTESIAN_POINT('Ctrl Pts',(8.43143566914408,-2.84862442585767,-1.5071351773836));
#6453=CARTESIAN_POINT('Origin',(13.3346225254169,0.,0.));
#6454=CARTESIAN_POINT('Ctrl Pts',(9.48780938168962,-2.84862442585767,1.50713517738359));
#6455=CARTESIAN_POINT('Ctrl Pts',(9.4646169756685,-2.67292600124808,1.83922139727825));
#6456=CARTESIAN_POINT('Ctrl Pts',(9.44281367098766,-2.44051109828623,2.1380390692589));
#6457=CARTESIAN_POINT('Ctrl Pts',(9.39642643037003,-1.88504609426699,2.64045772260141));
#6458=CARTESIAN_POINT('Ctrl Pts',(9.37216496812315,-1.56690035294904,2.84080649580198));
#6459=CARTESIAN_POINT('Ctrl Pts',(9.32261215620681,-0.833897623979761,3.14106096914872));
#6460=CARTESIAN_POINT('Ctrl Pts',(9.29881232552417,-0.418940672627908,3.22275695513633));
#6461=CARTESIAN_POINT('Ctrl Pts',(9.24717000287363,0.419039295201162,3.22274304415726));
#6462=CARTESIAN_POINT('Ctrl Pts',(9.21973240775526,0.833990015237942,3.14103793817188));
#6463=CARTESIAN_POINT('Ctrl Pts',(9.17128995711388,1.56698939071643,2.84075682635676));
#6464=CARTESIAN_POINT('Ctrl Pts',(9.14981109602737,1.88511415633464,2.64040452587235));
#6465=CARTESIAN_POINT('Ctrl Pts',(9.10383285405132,2.44054228571856,2.13800243635496));
#6466=CARTESIAN_POINT('Ctrl Pts',(9.07962631119985,2.67293936449861,1.83919613950281));
#6467=CARTESIAN_POINT('Ctrl Pts',(9.05643566914408,2.84862442585766,1.50713517738361));
#6468=CARTESIAN_POINT('Ctrl Pts',(9.24126248314343,-2.84862442585767,1.50713517738359));
#6469=CARTESIAN_POINT('Ctrl Pts',(9.21807174122128,-2.67293860794215,1.83919756946426));
#6470=CARTESIAN_POINT('Ctrl Pts',(9.19386717359377,-2.44054027367612,2.13800502293484));
#6471=CARTESIAN_POINT('Ctrl Pts',(9.14789222461089,-1.88510938726485,2.64040807821378));
#6472=CARTESIAN_POINT('Ctrl Pts',(9.12641453748589,-1.56698333133364,2.84076029566696));
#6473=CARTESIAN_POINT('Ctrl Pts',(9.07797229763274,-0.833984702087806,3.14103900650164));
#6474=CARTESIAN_POINT('Ctrl Pts',(9.05053411659157,-0.419036471460086,3.22274308756608));
#6475=CARTESIAN_POINT('Ctrl Pts',(8.99889267102348,0.418938503628748,3.22275691173686));
#6476=CARTESIAN_POINT('Ctrl Pts',(8.97509426960511,0.833892949681618,3.14106186836253));
#6477=CARTESIAN_POINT('Ctrl Pts',(8.92554134949045,1.56689486505516,2.84080964819597));
#6478=CARTESIAN_POINT('Ctrl Pts',(8.90127820754495,1.88504175038528,2.64046094274164));
#6479=CARTESIAN_POINT('Ctrl Pts',(8.85488685261699,2.44050915347968,2.13804154202824));
#6480=CARTESIAN_POINT('Ctrl Pts',(8.83308127592298,2.67292524895216,1.83922281918689));
#6481=CARTESIAN_POINT('Ctrl Pts',(8.80988877059788,2.84862442585767,1.50713517738359));
#6482=CARTESIAN_POINT('Origin',(13.3346225254169,0.,0.));
#6483=CARTESIAN_POINT('Ctrl Pts',(9.86626248314343,2.84862442585767,-1.50713517738359));
#6484=CARTESIAN_POINT('Ctrl Pts',(9.84307180085188,2.67293905968497,-1.83919671562868));
#6485=CARTESIAN_POINT('Ctrl Pts',(9.81886605820617,2.44054147501838,-2.13800347861122));
#6486=CARTESIAN_POINT('Ctrl Pts',(9.77288915678148,1.88511224339947,-2.64040594932443));
#6487=CARTESIAN_POINT('Ctrl Pts',(9.75141077761425,1.56698696950969,-2.84075821144642));
#6488=CARTESIAN_POINT('Ctrl Pts',(9.70296842516841,0.833987908650847,-3.14103835964394));
#6489=CARTESIAN_POINT('Ctrl Pts',(9.67553059684219,0.419038191995453,-3.22274305717364));
#6490=CARTESIAN_POINT('Ctrl Pts',(9.62388862676483,-0.418939765168384,-3.22275694212268));
#6491=CARTESIAN_POINT('Ctrl Pts',(9.60008936835002,-0.833895708774181,-3.14106133999854));
#6492=CARTESIAN_POINT('Ctrl Pts',(9.55053650011739,-1.56689811259611,-2.84080778192593));
#6493=CARTESIAN_POINT('Ctrl Pts',(9.52627435295588,-1.88504431610193,-2.64045903987891));
#6494=CARTESIAN_POINT('Ctrl Pts',(9.47988544172846,-2.44051030014507,-2.13804008421938));
#6495=CARTESIAN_POINT('Ctrl Pts',(9.45808121736454,-2.67292569257261,-1.83922198070335));
#6496=CARTESIAN_POINT('Ctrl Pts',(9.43488877059788,-2.84862442585766,-1.5071351773836));
#6497=CARTESIAN_POINT('Ctrl Pts',(10.1128093816896,2.84862442585767,-1.50713517738358));
#6498=CARTESIAN_POINT('Ctrl Pts',(10.0896170307097,2.67292641822307,-1.83922060915709));
#6499=CARTESIAN_POINT('Ctrl Pts',(10.0678149781225,2.44051217613953,-2.13803769870501));
#6500=CARTESIAN_POINT('Ctrl Pts',(10.021430022701,1.88504847411913,-2.64045596299845));
#6501=CARTESIAN_POINT('Ctrl Pts',(9.99716950323258,1.56690332970733,-2.84080478956146));
#6502=CARTESIAN_POINT('Ctrl Pts',(9.94761679526431,0.833900125799363,-3.1410604910179));
#6503=CARTESIAN_POINT('Ctrl Pts',(9.92381619849262,0.418941809982594,-3.222756984325));
#6504=CARTESIAN_POINT('Ctrl Pts',(9.87217340008585,-0.419040875537337,-3.22274301496216));
#6505=CARTESIAN_POINT('Ctrl Pts',(9.84473611394561,-0.8339929487316,-3.14103734546267));
#6506=CARTESIAN_POINT('Ctrl Pts',(9.79629350329155,-1.56699274015167,-2.840754911813));
#6507=CARTESIAN_POINT('Ctrl Pts',(9.77481397155242,-1.88511681315177,-2.64040255095991));
#6508=CARTESIAN_POINT('Ctrl Pts',(9.72883388836341,-2.44054341695358,-2.13800098192721));
#6509=CARTESIAN_POINT('Ctrl Pts',(9.70462625504794,-2.67293978988799,-1.83919533547766));
#6510=CARTESIAN_POINT('Ctrl Pts',(9.68143566914409,-2.84862442585767,-1.50713517738359));
#6511=CARTESIAN_POINT('Origin',(13.3346225254169,0.,0.));
#6512=CARTESIAN_POINT('Ctrl Pts',(10.7378093816897,-2.84862442585767,1.50713517738359));
#6513=CARTESIAN_POINT('Ctrl Pts',(10.7146170838525,-2.67292682081615,1.83921984821904));
#6514=CARTESIAN_POINT('Ctrl Pts',(10.6928162299734,-2.44051321684886,2.13803637525888));
#6515=CARTESIAN_POINT('Ctrl Pts',(10.6464334746689,-1.88505075481185,2.64045427966082));
#6516=CARTESIAN_POINT('Ctrl Pts',(10.6221738696468,-1.56690616308131,2.84080316794297));
#6517=CARTESIAN_POINT('Ctrl Pts',(10.5726212917232,-0.833902492085885,3.14106003933216));
#6518=CARTESIAN_POINT('Ctrl Pts',(10.5488199764818,-0.418942882035734,3.22275701285304));
#6519=CARTESIAN_POINT('Ctrl Pts',(10.497176727996,0.41904238163632,3.2227429864278));
#6520=CARTESIAN_POINT('Ctrl Pts',(10.4697397280512,0.833995737887798,3.14103678139506));
#6521=CARTESIAN_POINT('Ctrl Pts',(10.4212969337585,1.56699593640378,2.84075308716898));
#6522=CARTESIAN_POINT('Ctrl Pts',(10.3998167436331,1.88511936347304,2.64040065814822));
#6523=CARTESIAN_POINT('Ctrl Pts',(10.3538348794489,2.44054451029931,2.13799957609175));
#6524=CARTESIAN_POINT('Ctrl Pts',(10.3296262007761,2.67294020103435,1.83919455837315));
#6525=CARTESIAN_POINT('Ctrl Pts',(10.3064356691441,2.84862442585766,1.50713517738361));
#6526=CARTESIAN_POINT('Ctrl Pts',(10.4912624831434,-2.84862442585767,1.50713517738358));
#6527=CARTESIAN_POINT('Ctrl Pts',(10.4680718584017,-2.67293949566439,1.8391958915874));
#6528=CARTESIAN_POINT('Ctrl Pts',(10.443864991504,-2.44054263442528,2.13800198805734));
#6529=CARTESIAN_POINT('Ctrl Pts',(10.3978862041699,-1.88511497995812,2.6404039128587));
#6530=CARTESIAN_POINT('Ctrl Pts',(10.3764071455606,-1.56699043414843,2.84075622923762));
#6531=CARTESIAN_POINT('Ctrl Pts',(10.3279646515796,-0.833990950968164,3.14103774534431));
#6532=CARTESIAN_POINT('Ctrl Pts',(10.3005271495537,-0.419039828282384,3.22274302748307));
#6533=CARTESIAN_POINT('Ctrl Pts',(10.2488846843312,0.418940951798243,3.22275697180674));
#6534=CARTESIAN_POINT('Ctrl Pts',(10.225084623748,0.833898312837746,3.14106084191516));
#6535=CARTESIAN_POINT('Ctrl Pts',(10.1755318391322,1.56690119719985,2.84080601198241));
#6536=CARTESIAN_POINT('Ctrl Pts',(10.1512706556972,1.88504677018556,2.64045722310611));
#6537=CARTESIAN_POINT('Ctrl Pts',(10.1048840931523,2.44051140560248,2.13803867866086));
#6538=CARTESIAN_POINT('Ctrl Pts',(10.0830811609124,2.67292612023633,1.83922117237949));
#6539=CARTESIAN_POINT('Ctrl Pts',(10.0598887705979,2.84862442585767,1.50713517738359));
#6540=CARTESIAN_POINT('Origin',(13.3346225254169,0.,0.));
#6541=CARTESIAN_POINT('',(11.0234525205638,1.87154958983019,-2.62278522261047));
#6542=CARTESIAN_POINT('Ctrl Pts',(11.0230520901771,1.87192183080106,-2.62336162620986));
#6543=CARTESIAN_POINT('Ctrl Pts',(11.0079418888754,1.66946798355985,-2.76782427771551));
#6544=CARTESIAN_POINT('Ctrl Pts',(10.9932884442656,1.45097662306557,-2.88836270650252));
#6545=CARTESIAN_POINT('Ctrl Pts',(10.9632934504298,0.991158559414914,-3.07657202253502));
#6546=CARTESIAN_POINT('Ctrl Pts',(10.9476487851673,0.751458310552837,-3.14371789775113));
#6547=CARTESIAN_POINT('Ctrl Pts',(10.905150297864,0.0912513489784357,-3.24878003151173));
#6548=CARTESIAN_POINT('Ctrl Pts',(10.8795320204101,-0.332960972250965,-3.232971873478));
#6549=CARTESIAN_POINT('Ctrl Pts',(10.8417942436161,-0.945997583469522,-3.08789051095225));
#6550=CARTESIAN_POINT('Ctrl Pts',(10.8292395318735,-1.14458398877081,-3.01991762265664));
#6551=CARTESIAN_POINT('Ctrl Pts',(10.7939402148955,-1.65629153641311,-2.7869856969747));
#6552=CARTESIAN_POINT('Ctrl Pts',(10.7711998614304,-1.95124147240243,-2.58907215729383));
#6553=CARTESIAN_POINT('Ctrl Pts',(10.7274837181104,-2.46648776794441,-2.10434252694404));
#6554=CARTESIAN_POINT('Ctrl Pts',(10.7067726755519,-2.68283879666383,-1.82048530009627));
#6555=CARTESIAN_POINT('Ctrl Pts',(10.6848887705979,-2.84862442585766,-1.5071351773836));
#6556=CARTESIAN_POINT('',(11.0238490761438,-1.87158653173898,-2.62360084935061));
#6557=CARTESIAN_POINT('Origin',(11.0238490761438,0.,0.));
#6558=CARTESIAN_POINT('Ctrl Pts',(11.0238490761438,-1.87158653173898,-2.62360084935061));
#6559=CARTESIAN_POINT('Ctrl Pts',(11.0084296939351,-2.07493204384538,-2.4785411609296));
#6560=CARTESIAN_POINT('Ctrl Pts',(10.99328545226,-2.26072639839162,-2.31033087287213));
#6561=CARTESIAN_POINT('Ctrl Pts',(10.962448845779,-2.58972688979184,-1.934380324523));
#6562=CARTESIAN_POINT('Ctrl Pts',(10.9468549948036,-2.7318124303945,-1.72792061753715));
#6563=CARTESIAN_POINT('Ctrl Pts',(10.9314356691441,-2.84862442585767,-1.5071351773836));
#6564=CARTESIAN_POINT('Ctrl Pts',(11.1008112312664,1.68942544263115,3.40346056344526));
#6565=CARTESIAN_POINT('Ctrl Pts',(11.0751571795589,2.12830620414844,3.18560690803575));
#6566=CARTESIAN_POINT('Ctrl Pts',(11.0495031278513,2.52436782889846,2.88189967479167));
#6567=CARTESIAN_POINT('Ctrl Pts',(11.0238490761438,2.84862442585767,2.51456577037539));
#6568=CARTESIAN_POINT('Ctrl Pts',(11.0751571795589,1.70918178686444,3.44326104044715));
#6569=CARTESIAN_POINT('Ctrl Pts',(11.0495031278513,2.15319487277031,3.22285977820035));
#6570=CARTESIAN_POINT('Ctrl Pts',(11.0238490761438,2.55388808977572,2.91560095605822));
#6571=CARTESIAN_POINT('Ctrl Pts',(10.9981950244362,2.88193658236276,2.54397140480186));
#6572=CARTESIAN_POINT('Ctrl Pts',(11.0495031278513,1.72893813109773,3.48306151744904));
#6573=CARTESIAN_POINT('Ctrl Pts',(11.0238490761438,2.17808354139218,3.26011264836494));
#6574=CARTESIAN_POINT('Ctrl Pts',(10.9981950244362,2.58340835065299,2.94930223732478));
#6575=CARTESIAN_POINT('Ctrl Pts',(10.9725409727286,2.91524873886784,2.57337703922832));
#6576=CARTESIAN_POINT('Ctrl Pts',(11.0238490761438,1.74869447533101,3.52286199445093));
#6577=CARTESIAN_POINT('Ctrl Pts',(10.9981950244362,2.20297221001404,3.29736551852953));
#6578=CARTESIAN_POINT('Ctrl Pts',(10.9725409727286,2.61292861153025,2.98300351859134));
#6579=CARTESIAN_POINT('Ctrl Pts',(10.9468869210211,2.94856089537293,2.60278267365479));
#6580=CARTESIAN_POINT('',(11.0238490761438,1.74869447533103,3.52286199445092));
#6581=CARTESIAN_POINT('Ctrl Pts',(11.0238490761438,1.74869447533103,3.52286199445092));
#6582=CARTESIAN_POINT('Ctrl Pts',(11.0006887763626,2.15881326042978,3.31928534147352));
#6583=CARTESIAN_POINT('Ctrl Pts',(10.9775284765815,2.53280859423868,3.0432801490367));
#6584=CARTESIAN_POINT('Ctrl Pts',(10.9543681768003,2.84860418144656,2.71177492056083));
#6585=CARTESIAN_POINT('Origin',(11.0238490761448,0.32028972767158,0.987026521741422));
#6586=CARTESIAN_POINT('Ctrl Pts',(3.61729894227909,2.84735487989943,-1.50582500201333));
#6587=CARTESIAN_POINT('Ctrl Pts',(3.56935691049898,2.48448123509701,-2.19199227724466));
#6588=CARTESIAN_POINT('Ctrl Pts',(3.47348446621381,1.24430262445242,-3.28807336521129));
#6589=CARTESIAN_POINT('Ctrl Pts',(3.32966999014855,-1.2443026244524,-3.28807336521131));
#6590=CARTESIAN_POINT('Ctrl Pts',(3.23379754586339,-2.484481235097,-2.19199227724467));
#6591=CARTESIAN_POINT('Ctrl Pts',(3.18585551408329,-2.84735487989942,-1.50582500201335));
#6592=CARTESIAN_POINT('Ctrl Pts',(3.48027739894494,3.0571514143775,-1.6167760004937));
#6593=CARTESIAN_POINT('Ctrl Pts',(3.43233536716482,2.66754080269033,-2.35350090639904));
#6594=CARTESIAN_POINT('Ctrl Pts',(3.33646292287966,1.33598433939948,-3.53034256811279));
#6595=CARTESIAN_POINT('Ctrl Pts',(3.1926484468144,-1.33598433939945,-3.53034256811281));
#6596=CARTESIAN_POINT('Ctrl Pts',(3.09677600252924,-2.66754080269031,-2.35350090639906));
#6597=CARTESIAN_POINT('Ctrl Pts',(3.04883397074914,-3.05715141437748,-1.61677600049373));
#6598=CARTESIAN_POINT('Ctrl Pts',(3.34325585561077,3.26694794885555,-1.72772699897407));
#6599=CARTESIAN_POINT('Ctrl Pts',(3.29531382383067,2.85060037028365,-2.5150095355534));
#6600=CARTESIAN_POINT('Ctrl Pts',(3.19944137954551,1.42766605434656,-3.7726117710143));
#6601=CARTESIAN_POINT('Ctrl Pts',(3.05562690348025,-1.42766605434652,-3.77261177101431));
#6602=CARTESIAN_POINT('Ctrl Pts',(2.95975445919508,-2.85060037028362,-2.51500953555344));
#6603=CARTESIAN_POINT('Ctrl Pts',(2.91181242741498,-3.26694794885553,-1.7277269989741));
#6604=CARTESIAN_POINT('Ctrl Pts',(3.20623431227662,3.47674448333362,-1.83867799745444));
#6605=CARTESIAN_POINT('Ctrl Pts',(3.15829228049652,3.03365993787697,-2.67651816470778));
#6606=CARTESIAN_POINT('Ctrl Pts',(3.06241983621135,1.51934776929363,-4.01488097391579));
#6607=CARTESIAN_POINT('Ctrl Pts',(2.91860536014609,-1.51934776929357,-4.01488097391582));
#6608=CARTESIAN_POINT('Ctrl Pts',(2.82273291586093,-3.03365993787694,-2.67651816470782));
#6609=CARTESIAN_POINT('Ctrl Pts',(2.77479088408083,-3.47674448333358,-1.83867799745449));
#6610=CARTESIAN_POINT('',(3.02384926683068,0.656743230768742,-3.87731376376925));
#6611=CARTESIAN_POINT('Ctrl Pts',(3.02384907614375,0.656739510617936,-3.8773143808427));
#6612=CARTESIAN_POINT('Ctrl Pts',(3.02384907614375,0.535250361064991,-3.88669383362235));
#6613=CARTESIAN_POINT('Ctrl Pts',(3.02384907614375,0.413571786056566,-3.89044850980063));
#6614=CARTESIAN_POINT('Ctrl Pts',(3.02384907614375,0.292110717075194,-3.8886442850087));
#6615=CARTESIAN_POINT('Ctrl Pts',(3.02384907614375,0.170355995076364,-3.88683569819313));
#6616=CARTESIAN_POINT('Ctrl Pts',(3.02384907614374,0.048818954209201,-3.87944114113221));
#6617=CARTESIAN_POINT('Ctrl Pts',(3.02384907614374,-0.0720841978754196,
-3.86647526034617));
#6618=CARTESIAN_POINT('Ctrl Pts',(3.02384907614375,-0.190730889068619,-3.85375136665815));
#6619=CARTESIAN_POINT('Ctrl Pts',(3.02384907614375,-0.308767876865074,-3.83566186702548));
#6620=CARTESIAN_POINT('Ctrl Pts',(3.02384907614376,-0.425783805159,-3.81217453465478));
#6621=CARTESIAN_POINT('Ctrl Pts',(3.02384907614375,-0.503663329837124,-3.79654262618167));
#6622=CARTESIAN_POINT('Ctrl Pts',(3.02384907614375,-0.581090187929004,-3.77851880324373));
#6623=CARTESIAN_POINT('Ctrl Pts',(3.02384907614375,-0.657936143484074,-3.75808285085038));
#6624=CARTESIAN_POINT('Ctrl Pts',(3.02384907614375,-0.701243993343972,-3.74656582107826));
#6625=CARTESIAN_POINT('Ctrl Pts',(3.02384907614375,-0.744367230920925,-3.73428252775787));
#6626=CARTESIAN_POINT('Ctrl Pts',(3.02384907614375,-0.787281908740254,-3.72122819370286));
#6627=CARTESIAN_POINT('Ctrl Pts',(3.02384907614375,-0.813645800332897,-3.71320848889955));
#6628=CARTESIAN_POINT('Ctrl Pts',(3.02384907614375,-0.839937635499688,-3.7048954060654));
#6629=CARTESIAN_POINT('Ctrl Pts',(3.02384907614375,-0.866109900983181,-3.69630194449922));
#6630=CARTESIAN_POINT('Ctrl Pts',(3.02384907614375,-0.977678019052361,-3.65966941319454));
#6631=CARTESIAN_POINT('Ctrl Pts',(3.02384907614375,-1.08720975521468,-3.61790757563285));
#6632=CARTESIAN_POINT('Ctrl Pts',(3.02384907614375,-1.1943262208367,-3.57102425033263));
#6633=CARTESIAN_POINT('Ctrl Pts',(3.02384907614375,-1.23891450694224,-3.55150860341573));
#6634=CARTESIAN_POINT('Ctrl Pts',(3.02384907614375,-1.28308403622502,-3.53110498594551));
#6635=CARTESIAN_POINT('Ctrl Pts',(3.02384907614375,-1.32680617741716,-3.50981161930699));
#6636=CARTESIAN_POINT('Ctrl Pts',(3.02384907614375,-1.43289130004467,-3.45814650526161));
#6637=CARTESIAN_POINT('Ctrl Pts',(3.02384907614375,-1.53634510039748,-3.40124585112717));
#6638=CARTESIAN_POINT('Ctrl Pts',(3.02384907614375,-1.6368809757992,-3.33940450460461));
#6639=CARTESIAN_POINT('Ctrl Pts',(3.02384907614375,-1.73706849226998,-3.27777743965345));
#6640=CARTESIAN_POINT('Ctrl Pts',(3.02384907614375,-1.83435879667051,-3.21124313841696));
#6641=CARTESIAN_POINT('Ctrl Pts',(3.02384907614375,-1.92842806804127,-3.14006162188339));
#6642=CARTESIAN_POINT('Ctrl Pts',(3.02384907614375,-1.98023292809871,-3.10086127038747));
#6643=CARTESIAN_POINT('Ctrl Pts',(3.02384907614375,-2.0310601552513,-3.06025100909125));
#6644=CARTESIAN_POINT('Ctrl Pts',(3.02384907614375,-2.0808495508829,-3.018271330865));
#6645=CARTESIAN_POINT('Ctrl Pts',(3.02384907614375,-2.10068222578663,-3.00154951088178));
#6646=CARTESIAN_POINT('Ctrl Pts',(3.02384907614375,-2.12033510199989,-2.98462300334751));
#6647=CARTESIAN_POINT('Ctrl Pts',(3.02384907614375,-2.13979707289648,-2.96750248510467));
#6648=CARTESIAN_POINT('Ctrl Pts',(3.02384907614375,-2.22653562887142,-2.89119936874417));
#6649=CARTESIAN_POINT('Ctrl Pts',(3.02384907614375,-2.30953913984263,-2.81099999949489));
#6650=CARTESIAN_POINT('Ctrl Pts',(3.02384907614375,-2.3885507954711,-2.72719596287315));
#6651=CARTESIAN_POINT('Ctrl Pts',(3.02384907614375,-2.46682747261444,-2.64417148419631));
#6652=CARTESIAN_POINT('Ctrl Pts',(3.02384907614375,-2.5411866444644,-2.55760835213176));
#6653=CARTESIAN_POINT('Ctrl Pts',(3.02384907614375,-2.61133671528648,-2.46776198450897));
#6654=CARTESIAN_POINT('Ctrl Pts',(3.02384907614375,-2.68107943019947,-2.37843734763188));
#6655=CARTESIAN_POINT('Ctrl Pts',(3.02384907614376,-2.7466622109697,-2.28586682986901));
#6656=CARTESIAN_POINT('Ctrl Pts',(3.02384907614376,-2.80775053351277,-2.19028389748535));
#6657=CARTESIAN_POINT('Ctrl Pts',(3.02384907614376,-2.82131446704314,-2.16906084719493));
#6658=CARTESIAN_POINT('Ctrl Pts',(3.02384907614375,-2.8346566170922,-2.14768923548601));
#6659=CARTESIAN_POINT('Ctrl Pts',(3.02384907614375,-2.84777296580223,-2.12617155036607));
#6660=CARTESIAN_POINT('Ctrl Pts',(3.15165719587644,2.84680317627431,-2.71057532546662));
#6661=CARTESIAN_POINT('Ctrl Pts',(3.12190753622973,2.44054601589642,-3.13625204053632));
#6662=CARTESIAN_POINT('Ctrl Pts',(3.07930489321447,1.72451193341724,-3.61812485237549));
#6663=CARTESIAN_POINT('Ctrl Pts',(3.03670225019923,0.907494732982598,-3.83572067768669));
#6664=CARTESIAN_POINT('Ctrl Pts',(3.02384926683068,0.656743230768742,-3.87731376376925));
#6665=CARTESIAN_POINT('Ctrl Pts',(4.86728743325252,2.84737399657633,-1.50583210302806));
#6666=CARTESIAN_POINT('Ctrl Pts',(4.81934534671256,2.48449826149224,-2.19200478877887));
#6667=CARTESIAN_POINT('Ctrl Pts',(4.72347284766753,1.24425292797664,-3.2880767251413));
#6668=CARTESIAN_POINT('Ctrl Pts',(4.57965826208255,-1.24425292797662,-3.28807672514131));
#6669=CARTESIAN_POINT('Ctrl Pts',(4.48378576303753,-2.48449826149223,-2.19200478877888));
#6670=CARTESIAN_POINT('Ctrl Pts',(4.43584367649757,-2.84737399657632,-1.50583210302808));
#6671=CARTESIAN_POINT('Ctrl Pts',(4.73026978102042,3.05716466492174,-1.61677977751342));
#6672=CARTESIAN_POINT('Ctrl Pts',(4.68232769448045,2.66755273603903,-2.35350873950932));
#6673=CARTESIAN_POINT('Ctrl Pts',(4.58645519543543,1.33592780232221,-3.53033777499559));
#6674=CARTESIAN_POINT('Ctrl Pts',(4.44264060985045,-1.33592780232218,-3.5303377749956));
#6675=CARTESIAN_POINT('Ctrl Pts',(4.34676811080543,-2.66755273603901,-2.35350873950934));
#6676=CARTESIAN_POINT('Ctrl Pts',(4.29882602426546,-3.05716466492172,-1.61677977751345));
#6677=CARTESIAN_POINT('Ctrl Pts',(4.5932521287883,3.26695533326716,-1.72772745199879));
#6678=CARTESIAN_POINT('Ctrl Pts',(4.54531004224834,2.85060721058582,-2.51501269023978));
#6679=CARTESIAN_POINT('Ctrl Pts',(4.44943754320332,1.42760267666778,-3.77259882484987));
#6680=CARTESIAN_POINT('Ctrl Pts',(4.30562295761834,-1.42760267666773,-3.77259882484989));
#6681=CARTESIAN_POINT('Ctrl Pts',(4.20975045857331,-2.85060721058579,-2.51501269023981));
#6682=CARTESIAN_POINT('Ctrl Pts',(4.16180837203335,-3.26695533326714,-1.72772745199882));
#6683=CARTESIAN_POINT('Ctrl Pts',(4.4562344765562,3.47674600161257,-1.83867512648414));
#6684=CARTESIAN_POINT('Ctrl Pts',(4.40829239001624,3.03366168513261,-2.67651664097024));
#6685=CARTESIAN_POINT('Ctrl Pts',(4.31241989097121,1.51927755101335,-4.01485987470417));
#6686=CARTESIAN_POINT('Ctrl Pts',(4.16860530538623,-1.5192775510133,-4.01485987470418));
#6687=CARTESIAN_POINT('Ctrl Pts',(4.07273280634121,-3.03366168513258,-2.67651664097028));
#6688=CARTESIAN_POINT('Ctrl Pts',(4.02479071980125,-3.47674600161254,-1.83867512648419));
#6689=CARTESIAN_POINT('Ctrl Pts',(4.40165719587644,2.84679199383306,-2.71057163545836));
#6690=CARTESIAN_POINT('Ctrl Pts',(4.37190753622973,2.44052493609236,-3.13624479621667));
#6691=CARTESIAN_POINT('Ctrl Pts',(4.29422746407797,1.13490282761621,-4.01485987470402));
#6692=CARTESIAN_POINT('Ctrl Pts',(4.18679773227948,-1.13490282761596,-4.01485987470424));
#6693=CARTESIAN_POINT('Ctrl Pts',(4.10911766012771,-2.44052493609232,-3.1362447962167));
#6694=CARTESIAN_POINT('Ctrl Pts',(4.079368000481,-2.84679199383302,-2.7105716354584));
#6695=CARTESIAN_POINT('Ctrl Pts',(6.11727672162286,2.84739173784017,-1.50583878760475));
#6696=CARTESIAN_POINT('Ctrl Pts',(6.06933458598282,2.48451405189022,-2.19201646962288));
#6697=CARTESIAN_POINT('Ctrl Pts',(5.97346203783771,1.2442095628356,-3.28807951087694));
#6698=CARTESIAN_POINT('Ctrl Pts',(5.82964735405254,-1.24420956283556,-3.28807951087695));
#6699=CARTESIAN_POINT('Ctrl Pts',(5.73377480590744,-2.48451405189019,-2.19201646962291));
#6700=CARTESIAN_POINT('Ctrl Pts',(5.68583267026739,-2.84739173784015,-1.50583878760479));
#6701=CARTESIAN_POINT('Ctrl Pts',(5.98026268903406,3.0571769462154,-1.61678337581823));
#6702=CARTESIAN_POINT('Ctrl Pts',(5.93232055339401,2.66756378514623,-2.35351607142707));
#6703=CARTESIAN_POINT('Ctrl Pts',(5.83644800524891,1.33587828510277,-3.53033295151763));
#6704=CARTESIAN_POINT('Ctrl Pts',(5.69263332146373,-1.33587828510273,-3.53033295151765));
#6705=CARTESIAN_POINT('Ctrl Pts',(5.59676077331864,-2.6675637851462,-2.35351607142711));
#6706=CARTESIAN_POINT('Ctrl Pts',(5.54881863767859,-3.05717694621537,-1.61678337581828));
#6707=CARTESIAN_POINT('Ctrl Pts',(5.84324865644526,3.26696215459064,-1.72772796403172));
#6708=CARTESIAN_POINT('Ctrl Pts',(5.79530652080522,2.85061351840224,-2.51501567323129));
#6709=CARTESIAN_POINT('Ctrl Pts',(5.69943397266011,1.42754700736996,-3.77258639215831));
#6710=CARTESIAN_POINT('Ctrl Pts',(5.55561928887494,-1.42754700736989,-3.77258639215833));
#6711=CARTESIAN_POINT('Ctrl Pts',(5.45974674072984,-2.8506135184022,-2.51501567323134));
#6712=CARTESIAN_POINT('Ctrl Pts',(5.41180460508979,-3.26696215459061,-1.72772796403177));
#6713=CARTESIAN_POINT('Ctrl Pts',(5.70623462385646,3.47674736296587,-1.8386725522452));
#6714=CARTESIAN_POINT('Ctrl Pts',(5.65829248821641,3.03366325165824,-2.67651527503548));
#6715=CARTESIAN_POINT('Ctrl Pts',(5.56241994007131,1.51921572963714,-4.01483983279899));
#6716=CARTESIAN_POINT('Ctrl Pts',(5.41860525628614,-1.51921572963706,-4.01483983279902));
#6717=CARTESIAN_POINT('Ctrl Pts',(5.32273270814104,-3.03366325165819,-2.67651527503554));
#6718=CARTESIAN_POINT('Ctrl Pts',(5.27479057250099,-3.47674736296583,-1.83867255224527));
#6719=CARTESIAN_POINT('Ctrl Pts',(5.65165719587644,2.8467821456932,-2.71056813036079));
#6720=CARTESIAN_POINT('Ctrl Pts',(5.62190753622973,2.44050637155411,-3.13623791491845));
#6721=CARTESIAN_POINT('Ctrl Pts',(5.54422746407797,1.13485587203874,-4.01483983279886));
#6722=CARTESIAN_POINT('Ctrl Pts',(5.43679773227948,-1.13485587203849,-4.01483983279907));
#6723=CARTESIAN_POINT('Ctrl Pts',(5.35911766012771,-2.44050637155405,-3.1362379149185));
#6724=CARTESIAN_POINT('Ctrl Pts',(5.329368000481,-2.84678214569315,-2.71056813036084));
#6725=CARTESIAN_POINT('Ctrl Pts',(7.36726671258676,2.84740827328965,-1.50584509624218));
#6726=CARTESIAN_POINT('Ctrl Pts',(7.31932453261096,2.48452875995174,-2.19202741422533));
#6727=CARTESIAN_POINT('Ctrl Pts',(7.22345194013007,1.24417143185345,-3.28808183132752));
#6728=CARTESIAN_POINT('Ctrl Pts',(7.07963716767338,-1.24417143185342,-3.28808183132752));
#6729=CARTESIAN_POINT('Ctrl Pts',(6.98376457519251,-2.48452875995172,-2.19202741422535));
#6730=CARTESIAN_POINT('Ctrl Pts',(6.9358223952167,-2.84740827328965,-1.50584509624221));
#6731=CARTESIAN_POINT('Ctrl Pts',(7.2302560606791,3.05718837960027,-1.61678680675847));
#6732=CARTESIAN_POINT('Ctrl Pts',(7.18231388070327,2.66757406198433,-2.35352295678785));
#6733=CARTESIAN_POINT('Ctrl Pts',(7.0864412882224,1.33583458310969,-3.53032814444121));
#6734=CARTESIAN_POINT('Ctrl Pts',(6.94262651576571,-1.33583458310965,-3.53032814444122));
#6735=CARTESIAN_POINT('Ctrl Pts',(6.84675392328484,-2.6675740619843,-2.35352295678788));
#6736=CARTESIAN_POINT('Ctrl Pts',(6.79881174330904,-3.05718837960025,-1.6167868067585));
#6737=CARTESIAN_POINT('Ctrl Pts',(7.09324540877142,3.26696848591087,-1.72772851727475));
#6738=CARTESIAN_POINT('Ctrl Pts',(7.04530322879561,2.85061936401694,-2.51501849935038));
#6739=CARTESIAN_POINT('Ctrl Pts',(6.94943063631474,1.42749773436594,-3.7725744575549));
#6740=CARTESIAN_POINT('Ctrl Pts',(6.80561586385804,-1.42749773436588,-3.77257445755492));
#6741=CARTESIAN_POINT('Ctrl Pts',(6.70974327137717,-2.85061936401691,-2.51501849935041));
#6742=CARTESIAN_POINT('Ctrl Pts',(6.66180109140136,-3.26696848591084,-1.72772851727479));
#6743=CARTESIAN_POINT('Ctrl Pts',(6.95623475686376,3.47674859222147,-1.83867022779103));
#6744=CARTESIAN_POINT('Ctrl Pts',(6.90829257688794,3.03366466604953,-2.67651404191289));
#6745=CARTESIAN_POINT('Ctrl Pts',(6.81241998440707,1.51916088562219,-4.01482077066858));
#6746=CARTESIAN_POINT('Ctrl Pts',(6.66860521195038,-1.51916088562212,-4.01482077066861));
#6747=CARTESIAN_POINT('Ctrl Pts',(6.57273261946951,-3.03366466604949,-2.67651404191294));
#6748=CARTESIAN_POINT('Ctrl Pts',(6.5247904394937,-3.47674859222144,-1.83867022779109));
#6749=CARTESIAN_POINT('Ctrl Pts',(6.90165719587644,2.84677340648494,-2.71056479661449));
#6750=CARTESIAN_POINT('Ctrl Pts',(6.87190753622973,2.44048989744138,-3.13623137002149));
#6751=CARTESIAN_POINT('Ctrl Pts',(6.79422746407799,1.13481420380713,-4.01482077066858));
#6752=CARTESIAN_POINT('Ctrl Pts',(6.68679773227946,-1.13481420380722,-4.01482077066861));
#6753=CARTESIAN_POINT('Ctrl Pts',(6.60911766012771,-2.44048989744134,-3.13623137002152));
#6754=CARTESIAN_POINT('Ctrl Pts',(6.579368000481,-2.8467734064849,-2.71056479661452));
#6755=CARTESIAN_POINT('Ctrl Pts',(8.61725732794301,2.84742374204162,-1.50585106350619));
#6756=CARTESIAN_POINT('Ctrl Pts',(8.56931510768575,2.48454251156628,-2.19203770104955));
#6757=CARTESIAN_POINT('Ctrl Pts',(8.47344247492343,1.24413767428607,-3.2880837711184));
#6758=CARTESIAN_POINT('Ctrl Pts',(8.32962762190384,-1.24413767428604,-3.28808377111841));
#6759=CARTESIAN_POINT('Ctrl Pts',(8.23375498914152,-2.48454251156627,-2.19203770104957));
#6760=CARTESIAN_POINT('Ctrl Pts',(8.18581276888425,-2.84742374204161,-1.50585106350622));
#6761=CARTESIAN_POINT('Ctrl Pts',(8.48024984453137,3.05719906438292,-1.61679008096992));
#6762=CARTESIAN_POINT('Ctrl Pts',(8.43230762427411,2.66758365803813,-2.35352944129621));
#6763=CARTESIAN_POINT('Ctrl Pts',(8.33643499151179,1.33579575025379,-3.53032338680587));
#6764=CARTESIAN_POINT('Ctrl Pts',(8.1926201384922,-1.33579575025375,-3.53032338680589));
#6765=CARTESIAN_POINT('Ctrl Pts',(8.09674750572989,-2.66758365803811,-2.35352944129624));
#6766=CARTESIAN_POINT('Ctrl Pts',(8.04880528547262,-3.0571990643829,-1.61679008096995));
#6767=CARTESIAN_POINT('Ctrl Pts',(8.34324236111974,3.26697438672422,-1.72772909843364));
#6768=CARTESIAN_POINT('Ctrl Pts',(8.29530014086248,2.85062480450999,-2.51502118154286));
#6769=CARTESIAN_POINT('Ctrl Pts',(8.19942750810016,1.42745382622151,-3.77256300249335));
#6770=CARTESIAN_POINT('Ctrl Pts',(8.05561265508056,-1.42745382622146,-3.77256300249337));
#6771=CARTESIAN_POINT('Ctrl Pts',(7.95974002231824,-2.85062480450996,-2.5150211815429));
#6772=CARTESIAN_POINT('Ctrl Pts',(7.91179780206098,-3.2669743867242,-1.72772909843368));
#6773=CARTESIAN_POINT('Ctrl Pts',(8.20623487770811,3.47674970906552,-1.83866811589737));
#6774=CARTESIAN_POINT('Ctrl Pts',(8.15829265745084,3.03366595098184,-2.67651292178951));
#6775=CARTESIAN_POINT('Ctrl Pts',(8.06242002468851,1.51911190218921,-4.01480261818081));
#6776=CARTESIAN_POINT('Ctrl Pts',(7.91860517166893,-1.51911190218915,-4.01480261818084));
#6777=CARTESIAN_POINT('Ctrl Pts',(7.82273253890661,-3.0336659509818,-2.67651292178956));
#6778=CARTESIAN_POINT('Ctrl Pts',(7.77479031864935,-3.47674970906549,-1.83866811589743));
#6779=CARTESIAN_POINT('Ctrl Pts',(8.15165719587644,2.84676559888789,-2.71056162195416));
#6780=CARTESIAN_POINT('Ctrl Pts',(8.12190753622973,2.44047517949096,-3.13622513744625));
#6781=CARTESIAN_POINT('Ctrl Pts',(8.04422746407799,1.13477697746454,-4.0148026181808));
#6782=CARTESIAN_POINT('Ctrl Pts',(7.93679773227946,-1.13477697746461,-4.01480261818084));
#6783=CARTESIAN_POINT('Ctrl Pts',(7.85911766012771,-2.44047517949091,-3.13622513744629));
#6784=CARTESIAN_POINT('Ctrl Pts',(7.829368000481,-2.84676559888785,-2.71056162195421));
#6785=CARTESIAN_POINT('Ctrl Pts',(9.86724850229305,2.84743825981283,-1.50585671923049));
#6786=CARTESIAN_POINT('Ctrl Pts',(9.81930624523776,2.48455541132411,-2.19204739615685));
#6787=CARTESIAN_POINT('Ctrl Pts',(9.72343357567744,1.24410760572175,-3.28808539684982));
#6788=CARTESIAN_POINT('Ctrl Pts',(9.57961864906181,-1.24410760572175,-3.28808539684982));
#6789=CARTESIAN_POINT('Ctrl Pts',(9.48374597950147,-2.48455541132411,-2.19204739615685));
#6790=CARTESIAN_POINT('Ctrl Pts',(9.4358037224462,-2.84743825981283,-1.50585671923049));
#6791=CARTESIAN_POINT('Ctrl Pts',(9.73024399756275,3.0572090829841,-1.61679320836503));
#6792=CARTESIAN_POINT('Ctrl Pts',(9.68230174050747,2.66759264911214,-2.35353556368343));
#6793=CARTESIAN_POINT('Ctrl Pts',(9.58642907094713,1.33576103338308,-3.53031870181354));
#6794=CARTESIAN_POINT('Ctrl Pts',(9.44261414433152,-1.33576103338307,-3.53031870181354));
#6795=CARTESIAN_POINT('Ctrl Pts',(9.34674147477118,-2.66759264911214,-2.35353556368344));
#6796=CARTESIAN_POINT('Ctrl Pts',(9.29879921771591,-3.0572090829841,-1.61679320836504));
#6797=CARTESIAN_POINT('Ctrl Pts',(9.59323949283245,3.26697990615537,-1.72772969749955));
#6798=CARTESIAN_POINT('Ctrl Pts',(9.54529723577717,2.85062988690018,-2.51502373121002));
#6799=CARTESIAN_POINT('Ctrl Pts',(9.44942456621684,1.42741446104443,-3.77255200677727));
#6800=CARTESIAN_POINT('Ctrl Pts',(9.30560963960122,-1.42741446104441,-3.77255200677727));
#6801=CARTESIAN_POINT('Ctrl Pts',(9.20973697004088,-2.85062988690017,-2.51502373121004));
#6802=CARTESIAN_POINT('Ctrl Pts',(9.1617947129856,-3.26697990615537,-1.72772969749957));
#6803=CARTESIAN_POINT('Ctrl Pts',(9.45623498810215,3.47675072932665,-1.83866618663408));
#6804=CARTESIAN_POINT('Ctrl Pts',(9.40829273104687,3.03366712468821,-2.6765118987366));
#6805=CARTESIAN_POINT('Ctrl Pts',(9.31242006148653,1.51906788870579,-4.014785311741));
#6806=CARTESIAN_POINT('Ctrl Pts',(9.16860513487091,-1.51906788870575,-4.01478531174101));
#6807=CARTESIAN_POINT('Ctrl Pts',(9.07273246531058,-3.03366712468819,-2.67651189873662));
#6808=CARTESIAN_POINT('Ctrl Pts',(9.02479020825531,-3.47675072932664,-1.8386661866341));
#6809=CARTESIAN_POINT('Ctrl Pts',(9.40165719587644,2.84675858147378,-2.71055859525787));
#6810=CARTESIAN_POINT('Ctrl Pts',(9.37190753622973,2.44046195109913,-3.1362191953578));
#6811=CARTESIAN_POINT('Ctrl Pts',(9.29422746407799,1.13474351868581,-4.01478531174101));
#6812=CARTESIAN_POINT('Ctrl Pts',(9.18679773227947,-1.13474351868577,-4.01478531174101));
#6813=CARTESIAN_POINT('Ctrl Pts',(9.10911766012771,-2.4404619510991,-3.13621919535782));
#6814=CARTESIAN_POINT('Ctrl Pts',(9.079368000481,-2.84675858147374,-2.7105585952579));
#6815=CARTESIAN_POINT('Ctrl Pts',(11.102826855619,2.7325876658857,-1.7059759760899));
#6816=CARTESIAN_POINT('Ctrl Pts',(11.0564761776969,2.33512269759968,-2.34262495894918));
#6817=CARTESIAN_POINT('Ctrl Pts',(10.9637748218525,1.07966271388233,-3.32492883043245));
#6818=CARTESIAN_POINT('Ctrl Pts',(10.8247124167047,-1.31450087230183,-3.2393423413749));
#6819=CARTESIAN_POINT('Ctrl Pts',(10.7320006894791,-2.49670104301917,-2.16966721227558));
#6820=CARTESIAN_POINT('Ctrl Pts',(10.6856396401757,-2.84766280119442,-1.50605642114679));
#6821=CARTESIAN_POINT('Ctrl Pts',(10.965701366658,2.93405695958231,-1.83175484103065));
#6822=CARTESIAN_POINT('Ctrl Pts',(10.9193506887358,2.50728753844033,-2.515342929453));
#6823=CARTESIAN_POINT('Ctrl Pts',(10.8266493328915,1.15926450932041,-3.57007048550964));
#6824=CARTESIAN_POINT('Ctrl Pts',(10.6875869277437,-1.41141690746236,-3.47817384226539));
#6825=CARTESIAN_POINT('Ctrl Pts',(10.594875200518,-2.6807787953959,-2.32963328629069));
#6826=CARTESIAN_POINT('Ctrl Pts',(10.5485141512146,-3.05761639953827,-1.6170955388387));
#6827=CARTESIAN_POINT('Ctrl Pts',(10.828575877697,3.13552625327892,-1.9575337059714));
#6828=CARTESIAN_POINT('Ctrl Pts',(10.7822251997748,2.67945237928098,-2.68806089995681));
#6829=CARTESIAN_POINT('Ctrl Pts',(10.6895238439304,1.23886630475848,-3.81521214058682));
#6830=CARTESIAN_POINT('Ctrl Pts',(10.5504614387827,-1.50833294262289,-3.71700534315589));
#6831=CARTESIAN_POINT('Ctrl Pts',(10.4577497115571,-2.86485654777264,-2.48959936030581));
#6832=CARTESIAN_POINT('Ctrl Pts',(10.4113886622536,-3.26756999788213,-1.72813465653059));
#6833=CARTESIAN_POINT('Ctrl Pts',(10.6914503887359,3.33699554697554,-2.08331257091215));
#6834=CARTESIAN_POINT('Ctrl Pts',(10.6450997108137,2.85161722012163,-2.86077887046062));
#6835=CARTESIAN_POINT('Ctrl Pts',(10.5523983549694,1.31846810019657,-4.060353795664));
#6836=CARTESIAN_POINT('Ctrl Pts',(10.4133359498216,-1.60524897778342,-3.95583684404638));
#6837=CARTESIAN_POINT('Ctrl Pts',(10.320624222596,-3.04893430014939,-2.64956543432092));
#6838=CARTESIAN_POINT('Ctrl Pts',(10.2742631732926,-3.47752359622599,-1.83917377422248));
#6839=CARTESIAN_POINT('Ctrl Pts',(10.6511271608452,2.84811859529839,-2.71144775012001));
#6840=CARTESIAN_POINT('Ctrl Pts',(10.6426113435813,2.73171713488881,-2.83319832190457));
#6841=CARTESIAN_POINT('Ctrl Pts',(10.6340983716353,2.60759935714515,-2.94754525934051));
#6842=CARTESIAN_POINT('Ctrl Pts',(10.625585572441,2.47683252453344,-3.05366724755375));
#6843=CARTESIAN_POINT('Ctrl Pts',(10.6218467434829,2.41939961564344,-3.10027611892081));
#6844=CARTESIAN_POINT('Ctrl Pts',(10.6181079136966,2.36068334109682,-3.14529863695637));
#6845=CARTESIAN_POINT('Ctrl Pts',(10.6143687919012,2.30077187014575,-3.1886646310268));
#6846=CARTESIAN_POINT('Ctrl Pts',(10.6089168023024,2.21341533715529,-3.25189630989463));
#6847=CARTESIAN_POINT('Ctrl Pts',(10.6034641426978,2.12351330806985,-3.31160904245313));
#6848=CARTESIAN_POINT('Ctrl Pts',(10.5981005515451,2.03127319304859,-3.36743710409997));
#6849=CARTESIAN_POINT('Ctrl Pts',(10.5974339725144,2.01980973046982,-3.37437533152289));
#6850=CARTESIAN_POINT('Ctrl Pts',(10.5967687691587,2.00831021126505,-3.38125352367139));
#6851=CARTESIAN_POINT('Ctrl Pts',(10.596105113731,1.9967750816594,-3.38807094926279));
#6852=CARTESIAN_POINT('Ctrl Pts',(10.5901000063047,1.89239909139864,-3.449758643416));
#6853=CARTESIAN_POINT('Ctrl Pts',(10.5841550208651,1.78516834568221,-3.50656836848592));
#6854=CARTESIAN_POINT('Ctrl Pts',(10.5781918261005,1.67557705661834,-3.55828266075338));
#6855=CARTESIAN_POINT('Ctrl Pts',(10.5722246358433,1.56591233859679,-3.6100316029151));
#6856=CARTESIAN_POINT('Ctrl Pts',(10.5662388498881,1.4538822869375,-3.65667878953976));
#6857=CARTESIAN_POINT('Ctrl Pts',(10.5601720413959,1.33997712745255,-3.69799569478362));
#6858=CARTESIAN_POINT('Ctrl Pts',(10.5579472993162,1.29820729052431,-3.71314689954221));
#6859=CARTESIAN_POINT('Ctrl Pts',(10.5557115288928,1.25618558336911,-3.72758169383098));
#6860=CARTESIAN_POINT('Ctrl Pts',(10.553461263821,1.21393717344435,-3.74129018761173));
#6861=CARTESIAN_POINT('Ctrl Pts',(10.5534608102716,1.21392865811811,-3.74129295061032));
#6862=CARTESIAN_POINT('Ctrl Pts',(10.5534603567216,1.21392014278266,-3.7412957135794));
#6863=CARTESIAN_POINT('Ctrl Pts',(10.553459903171,1.21391162743801,-3.74129847651897));
#6864=CARTESIAN_POINT('Ctrl Pts',(10.5474425313702,1.10093636793918,-3.77795510385333));
#6865=CARTESIAN_POINT('Ctrl Pts',(10.5413175017578,0.986208288849423,-3.80945458848442));
#6866=CARTESIAN_POINT('Ctrl Pts',(10.5351573209224,0.870232321763314,-3.83568283978526));
#6867=CARTESIAN_POINT('Ctrl Pts',(10.5290007304002,0.75432394847934,-3.86189580458086));
#6868=CARTESIAN_POINT('Ctrl Pts',(10.5228093348457,0.637169173319156,-3.88284400980358));
#6869=CARTESIAN_POINT('Ctrl Pts',(10.5166366967313,0.519271500073078,-3.898455756584));
#6870=CARTESIAN_POINT('Ctrl Pts',(10.5104664725844,0.401419933716071,-3.91406139799307));
#6871=CARTESIAN_POINT('Ctrl Pts',(10.5043151500659,0.282822465141323,-3.92433507136264));
#6872=CARTESIAN_POINT('Ctrl Pts',(10.4982820270001,0.163987241636089,-3.92912540483231));
#6873=CARTESIAN_POINT('Ctrl Pts',(10.4922501071092,0.0451757172244269,-3.93391478297444));
#6874=CARTESIAN_POINT('Ctrl Pts',(10.486242686869,-0.0738614654372977,-3.93338541360083));
#6875=CARTESIAN_POINT('Ctrl Pts',(10.4802349464414,-0.192642255022724,-3.92759735592231));
#6876=CARTESIAN_POINT('Ctrl Pts',(10.4742254144236,-0.311458466663116,-3.92180757216588));
#6877=CARTESIAN_POINT('Ctrl Pts',(10.4682155029908,-0.430024800662094,-3.91075526859723));
#6878=CARTESIAN_POINT('Ctrl Pts',(10.4622839172821,-0.547828062706187,-3.89431655465985));
#6879=CARTESIAN_POINT('Ctrl Pts',(10.4563515943019,-0.665645967208858,-3.87787579745826));
#6880=CARTESIAN_POINT('Ctrl Pts',(10.4504973814454,-0.782693714943688,-3.85604789527817));
#6881=CARTESIAN_POINT('Ctrl Pts',(10.4446463021523,-0.89847165460343,-3.82897684250146));
#6882=CARTESIAN_POINT('Ctrl Pts',(10.4387907650912,-1.01433780212464,-3.80188516507311));
#6883=CARTESIAN_POINT('Ctrl Pts',(10.4329380781062,-1.12893399373693,-3.76954177223671));
#6884=CARTESIAN_POINT('Ctrl Pts',(10.4270312817244,-1.24175748432463,-3.73207010560792));
#6885=CARTESIAN_POINT('Ctrl Pts',(10.4228594183156,-1.3214426743339,-3.70560454546858));
#6886=CARTESIAN_POINT('Ctrl Pts',(10.4186601428766,-1.40024358005016,-3.67658170501823));
#6887=CARTESIAN_POINT('Ctrl Pts',(10.4144092301524,-1.47798418218269,-3.64505946246045));
#6888=CARTESIAN_POINT('Ctrl Pts',(10.4144087763743,-1.47799248086676,-3.64505609751183));
#6889=CARTESIAN_POINT('Ctrl Pts',(10.4144083225956,-1.47800077953875,-3.64505273253473));
#6890=CARTESIAN_POINT('Ctrl Pts',(10.4144078688164,-1.47800907819868,-3.64504936752915));
#6891=CARTESIAN_POINT('Ctrl Pts',(10.4081994866578,-1.59154721528751,-3.59901103502734));
#6892=CARTESIAN_POINT('Ctrl Pts',(10.4018766600276,-1.70294647533206,-3.5475869456103));
#6893=CARTESIAN_POINT('Ctrl Pts',(10.3955144750265,-1.81172128060229,-3.49103629418496));
#6894=CARTESIAN_POINT('Ctrl Pts',(10.3891567721835,-1.92041945404185,-3.43452548268334));
#6895=CARTESIAN_POINT('Ctrl Pts',(10.3827601083259,-2.02649714329538,-3.37289561599235));
#6896=CARTESIAN_POINT('Ctrl Pts',(10.3763800404594,-2.12949887542201,-3.30643628014277));
#6897=CARTESIAN_POINT('Ctrl Pts',(10.3700031717913,-2.23244895873014,-3.24001026942378));
#6898=CARTESIAN_POINT('Ctrl Pts',(10.3637052866195,-2.33226726847003,-3.16866913269694));
#6899=CARTESIAN_POINT('Ctrl Pts',(10.357507269449,-2.42851430469666,-3.09276322709174));
#6900=CARTESIAN_POINT('Ctrl Pts',(10.3485264698033,-2.56797428440723,-2.98277712808411));
#6901=CARTESIAN_POINT('Ctrl Pts',(10.3395467174008,-2.70016255934201,-2.86349404392066));
#6902=CARTESIAN_POINT('Ctrl Pts',(10.3305630683185,-2.82393045013914,-2.73594564924192));
#6903=CARTESIAN_POINT('Ctrl Pts',(10.3299882949333,-2.83184911313627,-2.72778510980977));
#6904=CARTESIAN_POINT('Ctrl Pts',(10.3294135057467,-2.83973329278916,-2.71959072700772));
#6905=CARTESIAN_POINT('Ctrl Pts',(10.3288386995335,-2.84758268181463,-2.71136276737431));
#6906=CARTESIAN_POINT('Origin',(11.0238490761436,0.781229937496414,-0.42649944676949));
#6907=CARTESIAN_POINT('Ctrl Pts',(4.24229308138461,-2.84736462220321,1.50582860737967));
#6908=CARTESIAN_POINT('Ctrl Pts',(4.19435102145226,-2.48448991370969,2.19199864350045));
#6909=CARTESIAN_POINT('Ctrl Pts',(4.09847854901485,-1.24427690485953,3.28807512492806));
#6910=CARTESIAN_POINT('Ctrl Pts',(3.95466401664509,1.24427690485951,3.28807512492806));
#6911=CARTESIAN_POINT('Ctrl Pts',(3.85879154420768,2.48448991370968,2.19199864350047));
#6912=CARTESIAN_POINT('Ctrl Pts',(3.81084948427533,2.84736462220321,1.50582860737969));
#6913=CARTESIAN_POINT('Ctrl Pts',(4.10527351983419,-3.05715816943107,1.61677791207915));
#6914=CARTESIAN_POINT('Ctrl Pts',(4.05733145990184,-2.66754688786205,2.35350488943491));
#6915=CARTESIAN_POINT('Ctrl Pts',(3.96145898746443,-1.33595510566621,3.53034017894723));
#6916=CARTESIAN_POINT('Ctrl Pts',(3.81764445509467,1.33595510566618,3.53034017894724));
#6917=CARTESIAN_POINT('Ctrl Pts',(3.72177198265727,2.66754688786203,2.35350488943492));
#6918=CARTESIAN_POINT('Ctrl Pts',(3.67382992272492,3.05715816943106,1.61677791207918));
#6919=CARTESIAN_POINT('Ctrl Pts',(3.96825395828378,-3.26695171665892,1.72772721677864));
#6920=CARTESIAN_POINT('Ctrl Pts',(3.92031189835143,-2.8506038620144,2.51501113536934));
#6921=CARTESIAN_POINT('Ctrl Pts',(3.82443942591402,-1.42763330647289,3.77260523296638));
#6922=CARTESIAN_POINT('Ctrl Pts',(3.68062489354426,1.42763330647285,3.77260523296639));
#6923=CARTESIAN_POINT('Ctrl Pts',(3.58475242110685,2.85060386201438,2.51501113536938));
#6924=CARTESIAN_POINT('Ctrl Pts',(3.5368103611745,3.2669517166589,1.72772721677867));
#6925=CARTESIAN_POINT('Ctrl Pts',(3.83123439673337,-3.47674526388677,1.83867652147811));
#6926=CARTESIAN_POINT('Ctrl Pts',(3.78329233680102,-3.03366083616676,2.67651738130379));
#6927=CARTESIAN_POINT('Ctrl Pts',(3.68741986436361,-1.51931150727957,4.01487028698555));
#6928=CARTESIAN_POINT('Ctrl Pts',(3.54360533199384,1.51931150727952,4.01487028698557));
#6929=CARTESIAN_POINT('Ctrl Pts',(3.44773285955643,3.03366083616673,2.67651738130383));
#6930=CARTESIAN_POINT('Ctrl Pts',(3.39979079962409,3.47674526388675,1.83867652147816));
#6931=CARTESIAN_POINT('Ctrl Pts',(3.77665719587644,-2.84679740187303,2.71057345644603));
#6932=CARTESIAN_POINT('Ctrl Pts',(3.74690753622973,-2.44053513068406,3.13624837122676));
#6933=CARTESIAN_POINT('Ctrl Pts',(3.66922746407795,-1.1349286129563,4.01487028698564));
#6934=CARTESIAN_POINT('Ctrl Pts',(3.56179773227949,1.13492861295628,4.01487028698554));
#6935=CARTESIAN_POINT('Ctrl Pts',(3.48411766012771,2.44053513068398,3.13624837122682));
#6936=CARTESIAN_POINT('Ctrl Pts',(3.454368000481,2.84679740187295,2.71057345644611));
#6937=CARTESIAN_POINT('Ctrl Pts',(5.492281984131,-2.84738302772049,1.50583549468422));
#6938=CARTESIAN_POINT('Ctrl Pts',(5.44433987239449,-2.48450630084475,2.19201072670901));
#6939=CARTESIAN_POINT('Ctrl Pts',(5.34846734815293,-1.24423052896037,3.28807818231816));
#6940=CARTESIAN_POINT('Ctrl Pts',(5.20465271217485,1.24423052896033,3.28807818231818));
#6941=CARTESIAN_POINT('Ctrl Pts',(5.10878018793329,2.48450630084472,2.19201072670904));
#6942=CARTESIAN_POINT('Ctrl Pts',(5.06083807619678,2.84738302772047,1.50583549468426));
#6943=CARTESIAN_POINT('Ctrl Pts',(5.35526617346927,-3.05717091855179,1.61678159827943));
#6944=CARTESIAN_POINT('Ctrl Pts',(5.30732406173276,-2.66755836357639,2.35351246446573));
#6945=CARTESIAN_POINT('Ctrl Pts',(5.2114515374912,-1.33590224851384,3.53033536375158));
#6946=CARTESIAN_POINT('Ctrl Pts',(5.06763690151313,1.33590224851378,3.53033536375161));
#6947=CARTESIAN_POINT('Ctrl Pts',(4.97176437727157,2.66755836357635,2.35351246446577));
#6948=CARTESIAN_POINT('Ctrl Pts',(4.92382226553506,3.05717091855177,1.61678159827947));
#6949=CARTESIAN_POINT('Ctrl Pts',(5.21825036280756,-3.26695880938309,1.72772770187462));
#6950=CARTESIAN_POINT('Ctrl Pts',(5.17030825107105,-2.85061042630803,2.51501420222245));
#6951=CARTESIAN_POINT('Ctrl Pts',(5.07443572682949,-1.42757396806733,3.772592545185));
#6952=CARTESIAN_POINT('Ctrl Pts',(4.93062109085141,1.42757396806726,3.77259254518503));
#6953=CARTESIAN_POINT('Ctrl Pts',(4.83474856660984,2.85061042630798,2.5150142022225));
#6954=CARTESIAN_POINT('Ctrl Pts',(4.78680645487334,3.26695880938306,1.72772770187468));
#6955=CARTESIAN_POINT('Ctrl Pts',(5.08123455214584,-3.4767467002144,1.83867380546982));
#6956=CARTESIAN_POINT('Ctrl Pts',(5.03329244040933,-3.03366248903967,2.67651593997917));
#6957=CARTESIAN_POINT('Ctrl Pts',(4.93741991616776,-1.51924568762079,4.01484972661843));
#6958=CARTESIAN_POINT('Ctrl Pts',(4.79360528018969,1.51924568762071,4.01484972661846));
#6959=CARTESIAN_POINT('Ctrl Pts',(4.69773275594812,3.03366248903961,2.67651593997923));
#6960=CARTESIAN_POINT('Ctrl Pts',(4.64979064421162,3.47674670021436,1.83867380546989));
#6961=CARTESIAN_POINT('Ctrl Pts',(5.02665719587644,-2.84678691836037,2.71056986067545));
#6962=CARTESIAN_POINT('Ctrl Pts',(4.99690753622973,-2.44051536841681,3.13624131191695));
#6963=CARTESIAN_POINT('Ctrl Pts',(4.919227464078,-1.1348786279445,4.01484972661831));
#6964=CARTESIAN_POINT('Ctrl Pts',(4.81179773227947,1.13487862794425,4.0148497266185));
#6965=CARTESIAN_POINT('Ctrl Pts',(4.73411766012771,2.44051536841673,3.13624131191701));
#6966=CARTESIAN_POINT('Ctrl Pts',(4.704368000481,2.8467869183603,2.71056986067553));
#6967=CARTESIAN_POINT('Ctrl Pts',(6.74227163450666,-2.84740014697697,1.50584198663232));
#6968=CARTESIAN_POINT('Ctrl Pts',(6.69432947615129,-2.48452153278042,2.19202202872339));
#6969=CARTESIAN_POINT('Ctrl Pts',(6.59845690529086,-1.24418990160601,3.28808072348868));
#6970=CARTESIAN_POINT('Ctrl Pts',(6.45464217607506,1.24418990160599,3.28808072348869));
#6971=CARTESIAN_POINT('Ctrl Pts',(6.35876960521463,2.4845215327804,2.1920220287234));
#6972=CARTESIAN_POINT('Ctrl Pts',(6.31082744685926,2.84740014697696,1.50584198663235));
#6973=CARTESIAN_POINT('Ctrl Pts',(6.60525932033858,-3.05718276224204,1.61678511152717));
#6974=CARTESIAN_POINT('Ctrl Pts',(6.55731716198321,-2.66756901396511,2.35351956688725));
#6975=CARTESIAN_POINT('Ctrl Pts',(6.46144459112278,-1.33585577151278,3.53033054359509));
#6976=CARTESIAN_POINT('Ctrl Pts',(6.31762986190698,1.33585577151274,3.53033054359509));
#6977=CARTESIAN_POINT('Ctrl Pts',(6.22175729104655,2.66756901396509,2.35351956688727));
#6978=CARTESIAN_POINT('Ctrl Pts',(6.17381513269119,3.05718276224202,1.61678511152721));
#6979=CARTESIAN_POINT('Ctrl Pts',(6.4682470061705,-3.26696537750712,1.72772823642201));
#6980=CARTESIAN_POINT('Ctrl Pts',(6.42030484781513,-2.85061649514982,2.51501710505113));
#6981=CARTESIAN_POINT('Ctrl Pts',(6.3244322769547,-1.42752164141955,3.77258036370151));
#6982=CARTESIAN_POINT('Ctrl Pts',(6.1806175477389,1.42752164141951,3.77258036370152));
#6983=CARTESIAN_POINT('Ctrl Pts',(6.08474497687847,2.85061649514979,2.51501710505116));
#6984=CARTESIAN_POINT('Ctrl Pts',(6.0368028185231,3.2669653775071,1.72772823642205));
#6985=CARTESIAN_POINT('Ctrl Pts',(6.33123469200243,-3.4767479927722,1.83867136131686));
#6986=CARTESIAN_POINT('Ctrl Pts',(6.28329253364706,-3.03366397633451,2.676514643215));
#6987=CARTESIAN_POINT('Ctrl Pts',(6.18741996278662,-1.51918751132632,4.01483018380791));
#6988=CARTESIAN_POINT('Ctrl Pts',(6.04360523357082,1.51918751132626,4.01483018380792));
#6989=CARTESIAN_POINT('Ctrl Pts',(5.94773266271039,3.03366397633447,2.67651464321504));
#6990=CARTESIAN_POINT('Ctrl Pts',(5.89979050435502,3.47674799277217,1.83867136131692));
#6991=CARTESIAN_POINT('Ctrl Pts',(6.27665719587644,-2.84677764951821,2.71056644286375));
#6992=CARTESIAN_POINT('Ctrl Pts',(6.24690753622973,-2.44049789590145,3.13623460198065));
#6993=CARTESIAN_POINT('Ctrl Pts',(6.16922746407796,-1.13483443443749,4.01483018380789));
#6994=CARTESIAN_POINT('Ctrl Pts',(6.06179773227948,1.13483443443743,4.01483018380793));
#6995=CARTESIAN_POINT('Ctrl Pts',(5.98411766012771,2.44049789590139,3.13623460198069));
#6996=CARTESIAN_POINT('Ctrl Pts',(5.954368000481,2.84677764951816,2.71056644286381));
#6997=CARTESIAN_POINT('Ctrl Pts',(7.99226194656689,-2.84741613328985,1.50584812058205));
#6998=CARTESIAN_POINT('Ctrl Pts',(7.94431974598207,-2.48453574834069,2.19203263547465));
#6999=CARTESIAN_POINT('Ctrl Pts',(7.84844713289218,-1.24415405273242,3.28808284427961));
#7000=CARTESIAN_POINT('Ctrl Pts',(7.70463231921746,1.24415405273241,3.28808284427962));
#7001=CARTESIAN_POINT('Ctrl Pts',(7.60875970612758,2.48453574834068,2.19203263547466));
#7002=CARTESIAN_POINT('Ctrl Pts',(7.56081750554275,2.84741613328985,1.50584812058207));
#7003=CARTESIAN_POINT('Ctrl Pts',(7.85525290394152,-3.05719381006904,1.61678846281894));
#7004=CARTESIAN_POINT('Ctrl Pts',(7.8073107033567,-2.66757894004992,2.35352624658332));
#7005=CARTESIAN_POINT('Ctrl Pts',(7.71143809026681,-1.33581460901229,3.53032575779908));
#7006=CARTESIAN_POINT('Ctrl Pts',(7.5676232765921,1.33581460901226,3.5303257577991));
#7007=CARTESIAN_POINT('Ctrl Pts',(7.47175066350222,2.66757894004991,2.35352624658334));
#7008=CARTESIAN_POINT('Ctrl Pts',(7.42380846291739,3.05719381006903,1.61678846281896));
#7009=CARTESIAN_POINT('Ctrl Pts',(7.71824386131615,-3.26697148684823,1.72772880505582));
#7010=CARTESIAN_POINT('Ctrl Pts',(7.67030166073133,-2.85062213175916,2.51501985769196));
#7011=CARTESIAN_POINT('Ctrl Pts',(7.57442904764143,-1.42747516529217,3.77256867131854));
#7012=CARTESIAN_POINT('Ctrl Pts',(7.43061423396673,1.42747516529213,3.77256867131855));
#7013=CARTESIAN_POINT('Ctrl Pts',(7.33474162087684,2.85062213175914,2.51501985769199));
#7014=CARTESIAN_POINT('Ctrl Pts',(7.28679942029201,3.26697148684821,1.72772880505585));
#7015=CARTESIAN_POINT('Ctrl Pts',(7.58123481869079,-3.47674916362741,1.83866914729269));
#7016=CARTESIAN_POINT('Ctrl Pts',(7.53329261810597,-3.0336653234684,2.67651346880062));
#7017=CARTESIAN_POINT('Ctrl Pts',(7.43742000501609,-1.51913572157204,4.01481158483801));
#7018=CARTESIAN_POINT('Ctrl Pts',(7.29360519134137,1.51913572157199,4.01481158483803));
#7019=CARTESIAN_POINT('Ctrl Pts',(7.19773257825148,3.03366532346837,2.67651346880066));
#7020=CARTESIAN_POINT('Ctrl Pts',(7.14979037766666,3.47674916362739,1.83866914729274));
#7021=CARTESIAN_POINT('Ctrl Pts',(7.52665719587644,-2.84676939580033,2.71056319011889));
#7022=CARTESIAN_POINT('Ctrl Pts',(7.49690753622974,-2.44048233697729,3.13622821610778));
#7023=CARTESIAN_POINT('Ctrl Pts',(7.41922746407797,-1.13479508100687,4.01481158483798));
#7024=CARTESIAN_POINT('Ctrl Pts',(7.31179773227947,1.13479508100694,4.01481158483804));
#7025=CARTESIAN_POINT('Ctrl Pts',(7.23411766012771,2.44048233697723,3.13622821610782));
#7026=CARTESIAN_POINT('Ctrl Pts',(7.204368000481,2.84676939580028,2.71056319011894));
#7027=CARTESIAN_POINT('Ctrl Pts',(9.24225284891195,-2.84743111333128,1.50585392860498));
#7028=CARTESIAN_POINT('Ctrl Pts',(9.19431060985147,-2.48454906208509,2.19204261884696));
#7029=CARTESIAN_POINT('Ctrl Pts',(9.09843795828593,-1.24412221602484,3.2880846196523));
#7030=CARTESIAN_POINT('Ctrl Pts',(8.9546230676599,1.24412221602484,3.2880846196523));
#7031=CARTESIAN_POINT('Ctrl Pts',(8.85875041609436,2.48454906208509,2.19204261884696));
#7032=CARTESIAN_POINT('Ctrl Pts',(8.81080817703388,2.84743111333128,1.50585392860498));
#7033=CARTESIAN_POINT('Ctrl Pts',(9.10524687731388,-3.05720415235532,1.61679166242786));
#7034=CARTESIAN_POINT('Ctrl Pts',(9.0573046382534,-2.66758822497045,2.35353254556472));
#7035=CARTESIAN_POINT('Ctrl Pts',(8.96143198668786,-1.33577791822989,3.53032103408329));
#7036=CARTESIAN_POINT('Ctrl Pts',(8.81761709606184,1.33577791822988,3.53032103408329));
#7037=CARTESIAN_POINT('Ctrl Pts',(8.7217444444963,2.66758822497045,2.35353254556473));
#7038=CARTESIAN_POINT('Ctrl Pts',(8.67380220543582,3.05720415235531,1.61679166242787));
#7039=CARTESIAN_POINT('Ctrl Pts',(8.96824090571582,-3.26697719137936,1.72772939625073));
#7040=CARTESIAN_POINT('Ctrl Pts',(8.92029866665534,-2.85062738785583,2.51502247228247));
#7041=CARTESIAN_POINT('Ctrl Pts',(8.82442601508979,-1.42743362043492,3.77255744851429));
#7042=CARTESIAN_POINT('Ctrl Pts',(8.68061112446378,1.4274336204349,3.77255744851431));
#7043=CARTESIAN_POINT('Ctrl Pts',(8.58473847289823,2.85062738785582,2.51502247228249));
#7044=CARTESIAN_POINT('Ctrl Pts',(8.53679623383775,3.26697719137935,1.72772939625075));
#7045=CARTESIAN_POINT('Ctrl Pts',(8.83123493411776,-3.47675023040339,1.83866713007362));
#7046=CARTESIAN_POINT('Ctrl Pts',(8.78329269505728,-3.03366655074119,2.67651239900022));
#7047=CARTESIAN_POINT('Ctrl Pts',(8.68742004349173,-1.51908932263997,4.01479386294529));
#7048=CARTESIAN_POINT('Ctrl Pts',(8.54360515286572,1.51908932263994,4.0147938629453));
#7049=CARTESIAN_POINT('Ctrl Pts',(8.44773250130017,3.03366655074117,2.67651239900024));
#7050=CARTESIAN_POINT('Ctrl Pts',(8.39979026223969,3.47675023040338,1.83866713007365));
#7051=CARTESIAN_POINT('Ctrl Pts',(8.77665719587644,-2.84676199909996,2.71056009076467));
#7052=CARTESIAN_POINT('Ctrl Pts',(8.74690753622973,-2.44046839360025,3.13622213137543));
#7053=CARTESIAN_POINT('Ctrl Pts',(8.66922746407795,-1.13475981380474,4.01479386294536));
#7054=CARTESIAN_POINT('Ctrl Pts',(8.56179773227949,1.13475981380472,4.01479386294528));
#7055=CARTESIAN_POINT('Ctrl Pts',(8.48411766012771,2.4404683936002,3.13622213137546));
#7056=CARTESIAN_POINT('Ctrl Pts',(8.454368000481,2.84676199909991,2.71056009076472));
#7057=CARTESIAN_POINT('Ctrl Pts',(10.4922442814608,-2.84744519313275,1.50585943851893));
#7058=CARTESIAN_POINT('Ctrl Pts',(10.4443020071642,-2.48456156979463,2.19205203972627));
#7059=CARTESIAN_POINT('Ctrl Pts',(10.3484293203624,-1.24409377838615,3.28808610894595));
#7060=CARTESIAN_POINT('Ctrl Pts',(10.2046143592641,1.24409377838615,3.28808610894595));
#7061=CARTESIAN_POINT('Ctrl Pts',(10.1087416724623,2.48456156979462,2.19205203972627));
#7062=CARTESIAN_POINT('Ctrl Pts',(10.0607993981656,2.84744519313275,1.50585943851893));
#7063=CARTESIAN_POINT('Ctrl Pts',(10.3552412009161,-3.05721386454218,1.61679471991055));
#7064=CARTESIAN_POINT('Ctrl Pts',(10.3072989266194,-2.66759693805657,2.3535384996387));
#7065=CARTESIAN_POINT('Ctrl Pts',(10.2114262398176,-1.33574502408184,3.5303163918033));
#7066=CARTESIAN_POINT('Ctrl Pts',(10.0676112787192,1.33574502408182,3.53031639180331));
#7067=CARTESIAN_POINT('Ctrl Pts',(9.97173859191745,2.66759693805656,2.35353849963872));
#7068=CARTESIAN_POINT('Ctrl Pts',(9.92379631762076,3.05721386454217,1.61679471991057));
#7069=CARTESIAN_POINT('Ctrl Pts',(10.2182381203711,-3.26698253595159,1.7277300013022));
#7070=CARTESIAN_POINT('Ctrl Pts',(10.1702958460745,-2.8506323063185,2.51502495955112));
#7071=CARTESIAN_POINT('Ctrl Pts',(10.0744231592728,-1.42739626977752,3.77254667466065));
#7072=CARTESIAN_POINT('Ctrl Pts',(9.93060819817435,1.42739626977749,3.77254667466066));
#7073=CARTESIAN_POINT('Ctrl Pts',(9.83473551137261,2.85063230631848,2.51502495955114));
#7074=CARTESIAN_POINT('Ctrl Pts',(9.78679323707594,3.26698253595158,1.72773000130222));
#7075=CARTESIAN_POINT('Ctrl Pts',(10.0812350398263,-3.47675120736102,1.83866528269383));
#7076=CARTESIAN_POINT('Ctrl Pts',(10.0332927655296,-3.03366767458044,2.67651141946355));
#7077=CARTESIAN_POINT('Ctrl Pts',(9.93742007872794,-1.5190475154732,4.014776957518));
#7078=CARTESIAN_POINT('Ctrl Pts',(9.79360511762951,1.51904751547316,4.01477695751801));
#7079=CARTESIAN_POINT('Ctrl Pts',(9.69773243082778,3.03366767458041,2.67651141946358));
#7080=CARTESIAN_POINT('Ctrl Pts',(9.6497901565311,3.476751207361,1.83866528269385));
#7081=CARTESIAN_POINT('Ctrl Pts',(10.0266571958764,-2.84675533252353,2.71055713420083));
#7082=CARTESIAN_POINT('Ctrl Pts',(9.99690753622973,-2.44045582656577,3.13621632697281));
#7083=CARTESIAN_POINT('Ctrl Pts',(9.91922746407798,-1.13472802780763,4.01477695751801));
#7084=CARTESIAN_POINT('Ctrl Pts',(9.81179773227947,1.13472802780759,4.01477695751801));
#7085=CARTESIAN_POINT('Ctrl Pts',(9.73411766012771,2.44045582656573,3.13621632697284));
#7086=CARTESIAN_POINT('Ctrl Pts',(9.704368000481,2.84675533252349,2.71055713420087));
#7087=CARTESIAN_POINT('Origin',(3.02384907614375,0.,0.));
#7088=CARTESIAN_POINT('Ctrl Pts',(3.02384907614375,-0.0271982295007612,
3.22179557349031));
#7089=CARTESIAN_POINT('Ctrl Pts',(3.02384907614375,0.0787467680287735,3.23416676714299));
#7090=CARTESIAN_POINT('Ctrl Pts',(3.02384907614375,0.185048789657521,3.24132583932574));
#7091=CARTESIAN_POINT('Ctrl Pts',(3.02384907614375,0.291285361330346,3.24329345860347));
#7092=CARTESIAN_POINT('Ctrl Pts',(3.02384907614375,0.398696099786925,3.24528282475387));
#7093=CARTESIAN_POINT('Ctrl Pts',(3.02384907614375,0.506040779421253,3.24196569447197));
#7094=CARTESIAN_POINT('Ctrl Pts',(3.02384907614375,0.612908356448757,3.2333169334513));
#7095=CARTESIAN_POINT('Ctrl Pts',(3.02384907614375,0.69342764175655,3.22680053179279));
#7096=CARTESIAN_POINT('Ctrl Pts',(3.02384907614375,0.773676703283155,3.21725651226085));
#7097=CARTESIAN_POINT('Ctrl Pts',(3.02384907614375,0.853484633313019,3.204655194923));
#7098=CARTESIAN_POINT('Ctrl Pts',(3.02384907614375,0.948602940134056,3.18963643715743));
#7099=CARTESIAN_POINT('Ctrl Pts',(3.02384907614375,1.04309503128853,3.17027579824669));
#7100=CARTESIAN_POINT('Ctrl Pts',(3.02384907614375,1.13674268826726,3.14672432130043));
#7101=CARTESIAN_POINT('Ctrl Pts',(3.02384907614375,1.15921157599614,3.14107361408119));
#7102=CARTESIAN_POINT('Ctrl Pts',(3.02384907614375,1.18163183734146,3.13518149603407));
#7103=CARTESIAN_POINT('Ctrl Pts',(3.02384907614375,1.20400041713337,3.12904975582882));
#7104=CARTESIAN_POINT('Ctrl Pts',(3.02384907614375,1.22668855383874,3.12283041775225));
#7105=CARTESIAN_POINT('Ctrl Pts',(3.02384907614375,1.2493272800887,3.11636326663925));
#7106=CARTESIAN_POINT('Ctrl Pts',(3.02384907614375,1.27187893963435,3.10966082396874));
#7107=CARTESIAN_POINT('Ctrl Pts',(3.02384907614375,1.37566821123953,3.07881424075653));
#7108=CARTESIAN_POINT('Ctrl Pts',(3.02384907614376,1.4777658367785,3.04294833555469));
#7109=CARTESIAN_POINT('Ctrl Pts',(3.02384907614375,1.57787399170956,3.00235617548192));
#7110=CARTESIAN_POINT('Ctrl Pts',(3.02384907614375,1.67945971177358,2.96116488779126));
#7111=CARTESIAN_POINT('Ctrl Pts',(3.02384907614375,1.77899754429907,2.91510663434206));
#7112=CARTESIAN_POINT('Ctrl Pts',(3.02384907614375,1.87617830774079,2.86443319678252));
#7113=CARTESIAN_POINT('Ctrl Pts',(3.02384907614376,1.97420990059414,2.81331610710976));
#7114=CARTESIAN_POINT('Ctrl Pts',(3.02384907614375,2.06984379056666,2.75750242593435));
#7115=CARTESIAN_POINT('Ctrl Pts',(3.02384907614375,2.1627527754763,2.69719875952457));
#7116=CARTESIAN_POINT('Ctrl Pts',(3.02384907614375,2.22372524808531,2.65762386101535));
#7117=CARTESIAN_POINT('Ctrl Pts',(3.02384907614376,2.28352394250253,2.61611417188707));
#7118=CARTESIAN_POINT('Ctrl Pts',(3.02384907614376,2.3420514723285,2.57271690759621));
#7119=CARTESIAN_POINT('Ctrl Pts',(3.02384907614376,2.36251670760645,2.55754225001589));
#7120=CARTESIAN_POINT('Ctrl Pts',(3.02384907614375,2.38282647584896,2.54213672662517));
#7121=CARTESIAN_POINT('Ctrl Pts',(3.02384907614375,2.40297645819471,2.52650211691943));
#7122=CARTESIAN_POINT('Ctrl Pts',(3.02384907614375,2.41529317891841,2.51694542758514));
#7123=CARTESIAN_POINT('Ctrl Pts',(3.02384907614376,2.42754254591775,2.50730907271123));
#7124=CARTESIAN_POINT('Ctrl Pts',(3.02384907614376,2.43972290434691,2.49759447327989));
#7125=CARTESIAN_POINT('Ctrl Pts',(3.02384907614376,2.52887669074654,2.42648873959427));
#7126=CARTESIAN_POINT('Ctrl Pts',(3.02384907614376,2.61435347490571,2.35118026521884));
#7127=CARTESIAN_POINT('Ctrl Pts',(3.02384907614375,2.69583042051309,2.27193767966696));
#7128=CARTESIAN_POINT('Ctrl Pts',(3.02384907614375,2.74846100352769,2.22075039661297));
#7129=CARTESIAN_POINT('Ctrl Pts',(3.02384907614375,2.7994224920531,2.16792047499698));
#7130=CARTESIAN_POINT('Ctrl Pts',(3.02384907614375,2.84862442584919,2.11350930842726));
#7131=CARTESIAN_POINT('Origin',(3.02384907614375,0.,0.));
#7132=CARTESIAN_POINT('Origin',(11.0238490761438,0.,0.));
#7133=CARTESIAN_POINT('Origin',(11.0238490761438,0.,0.));
#7134=CARTESIAN_POINT('',(11.0238490761438,-1.74837398213582,3.52379982655521));
#7135=CARTESIAN_POINT('Ctrl Pts',(10.7710409564111,2.84675014301221,2.71055471688623));
#7136=CARTESIAN_POINT('Ctrl Pts',(10.8007906160578,2.44044604391822,3.13621158123827));
#7137=CARTESIAN_POINT('Ctrl Pts',(10.8784706882095,1.13470328440395,4.01476313548051));
#7138=CARTESIAN_POINT('Ctrl Pts',(10.9627400614538,-0.645450738027376,4.01476313548051));
#7139=CARTESIAN_POINT('Ctrl Pts',(11.0172597750513,-1.6320315860502,3.5819951336082));
#7140=CARTESIAN_POINT('Ctrl Pts',(11.0238490761438,-1.74837398213582,3.52379982655521));
#7141=CARTESIAN_POINT('Origin',(11.0238490761438,0.,0.));
#7142=CARTESIAN_POINT('Origin',(11.0238490761438,0.,0.));
#7143=CARTESIAN_POINT('Ctrl Pts',(3.27133852370579,2.84851080212945,2.71166475696575));
#7144=CARTESIAN_POINT('Ctrl Pts',(3.27756781179114,2.76510016696855,2.79918925385792));
#7145=CARTESIAN_POINT('Ctrl Pts',(3.2837527883943,2.67757721529466,2.88281756264117));
#7146=CARTESIAN_POINT('Ctrl Pts',(3.28986642234616,2.5863612587383,2.96220306305726));
#7147=CARTESIAN_POINT('Ctrl Pts',(3.29992445826663,2.43629447770612,3.09280659951976));
#7148=CARTESIAN_POINT('Ctrl Pts',(3.30998041189806,2.2764553229174,3.21217789614563));
#7149=CARTESIAN_POINT('Ctrl Pts',(3.32003847075117,2.10867580690382,3.31906420594094));
#7150=CARTESIAN_POINT('Ctrl Pts',(3.3222082142292,2.07248209239735,3.34212192283809));
#7151=CARTESIAN_POINT('Ctrl Pts',(3.32437805967445,2.03591869476326,3.36459853299068));
#7152=CARTESIAN_POINT('Ctrl Pts',(3.32654805148509,1.99900380615245,3.38648121755032));
#7153=CARTESIAN_POINT('Ctrl Pts',(3.33266414469029,1.89495968105666,3.44815727443238));
#7154=CARTESIAN_POINT('Ctrl Pts',(3.33865883462581,1.78801821896177,3.50493031843278));
#7155=CARTESIAN_POINT('Ctrl Pts',(3.34462164921526,1.67870528210083,3.55662383796714));
#7156=CARTESIAN_POINT('Ctrl Pts',(3.35058846331992,1.56931902436992,3.60835203055972));
#7157=CARTESIAN_POINT('Ctrl Pts',(3.35654216848938,1.45756904643851,3.65502441172559));
#7158=CARTESIAN_POINT('Ctrl Pts',(3.36253222850543,1.343938602328,3.69641849044391));
#7159=CARTESIAN_POINT('Ctrl Pts',(3.36827725878748,1.23495633159455,3.73611930063572));
#7160=CARTESIAN_POINT('Ctrl Pts',(3.37405616830194,1.12424439913972,3.77096467413984));
#7161=CARTESIAN_POINT('Ctrl Pts',(3.37992528781139,1.01225173346125,3.80079224580091));
#7162=CARTESIAN_POINT('Ctrl Pts',(3.37992569942838,1.01224387911722,3.80079433768798));
#7163=CARTESIAN_POINT('Ctrl Pts',(3.37992611104581,1.01223602476688,3.80079642955039));
#7164=CARTESIAN_POINT('Ctrl Pts',(3.37992652266369,1.01222817041023,3.80079852138812));
#7165=CARTESIAN_POINT('Ctrl Pts',(3.38595485692058,0.89719748284113,3.83143445295053));
#7166=CARTESIAN_POINT('Ctrl Pts',(3.39208264801567,0.780693546216728,3.8568063507963));
#7167=CARTESIAN_POINT('Ctrl Pts',(3.39824032428524,0.663227890410915,3.87682699648556));
#7168=CARTESIAN_POINT('Ctrl Pts',(3.40439467936307,0.545825590642329,3.89683684388007));
#7169=CARTESIAN_POINT('Ctrl Pts',(3.41057860191865,0.42746261603,3.9115015228185));
#7170=CARTESIAN_POINT('Ctrl Pts',(3.41674195624578,0.308647273882812,3.92077563304824));
#7171=CARTESIAN_POINT('Ctrl Pts',(3.42290313226368,0.189873924543737,3.93004646553688));
#7172=CARTESIAN_POINT('Ctrl Pts',(3.42904361208695,0.0706467335888831,3.93393067034779));
#7173=CARTESIAN_POINT('Ctrl Pts',(3.43510230316468,-0.0485226577253618,
3.93236313392551));
#7174=CARTESIAN_POINT('Ctrl Pts',(3.44115997878588,-0.167672075858033,3.9307958602275));
#7175=CARTESIAN_POINT('Ctrl Pts',(3.4471804649664,-0.286760773972386,3.92385631726269));
#7176=CARTESIAN_POINT('Ctrl Pts',(3.45320144088977,-0.405304115191476,3.91164518924961));
#7177=CARTESIAN_POINT('Ctrl Pts',(3.45922414139615,-0.523881410678953,3.89943056361352));
#7178=CARTESIAN_POINT('Ctrl Pts',(3.46519339328439,-0.641906978532429,3.88184752285106));
#7179=CARTESIAN_POINT('Ctrl Pts',(3.47110125638993,-0.75886370394298,3.85891687398524));
#7180=CARTESIAN_POINT('Ctrl Pts',(3.47700997128401,-0.875837292032086,3.83598291900633));
#7181=CARTESIAN_POINT('Ctrl Pts',(3.4828863611721,-0.99174991754334,3.80774905124001));
#7182=CARTESIAN_POINT('Ctrl Pts',(3.48877152714845,-1.10610013420366,3.77432248235088));
#7183=CARTESIAN_POINT('Ctrl Pts',(3.49466057807916,-1.22052583647876,3.74087384769593));
#7184=CARTESIAN_POINT('Ctrl Pts',(3.50055873183273,-1.33338691008093,3.70222533306509));
#7185=CARTESIAN_POINT('Ctrl Pts',(3.5065249803474,-1.44418417826052,3.6585283537727));
#7186=CARTESIAN_POINT('Ctrl Pts',(3.50889018855399,-1.48810769356856,3.64120549942439));
#7187=CARTESIAN_POINT('Ctrl Pts',(3.51126626796972,-1.53170691529297,3.62308975173028));
#7188=CARTESIAN_POINT('Ctrl Pts',(3.51365746934456,-1.57495099764014,3.60419264462701));
#7189=CARTESIAN_POINT('Ctrl Pts',(3.51365788148981,-1.57495845115016,3.60418938753912));
#7190=CARTESIAN_POINT('Ctrl Pts',(3.51365829363552,-1.57496590464962,3.60418613042802));
#7191=CARTESIAN_POINT('Ctrl Pts',(3.51365870578167,-1.57497335813855,3.6041828732937));
#7192=CARTESIAN_POINT('Ctrl Pts',(3.51989178432406,-1.68769594777398,3.55492371172874));
#7193=CARTESIAN_POINT('Ctrl Pts',(3.52623092322446,-1.79811199519124,3.50030287918353));
#7194=CARTESIAN_POINT('Ctrl Pts',(3.53260372599692,-1.90574025619246,3.44059439960986));
#7195=CARTESIAN_POINT('Ctrl Pts',(3.53897256246437,-2.0133015315163,3.38092308139987));
#7196=CARTESIAN_POINT('Ctrl Pts',(3.54537469806406,-2.11807877137534,3.31617070281869));
#7197=CARTESIAN_POINT('Ctrl Pts',(3.551757907507,-2.21962094813659,3.24664071361019));
#7198=CARTESIAN_POINT('Ctrl Pts',(3.55813816931474,-2.32111623480328,3.17714283192461));
#7199=CARTESIAN_POINT('Ctrl Pts',(3.56445359556647,-2.41933468255066,3.10280613901885));
#7200=CARTESIAN_POINT('Ctrl Pts',(3.57067623702516,-2.51383508889289,3.02397624789742));
#7201=CARTESIAN_POINT('Ctrl Pts',(3.57838709026876,-2.63093628612604,2.92629333852825));
#7202=CARTESIAN_POINT('Ctrl Pts',(3.58609768658623,-2.74248705096226,2.82190190265532));
#7203=CARTESIAN_POINT('Ctrl Pts',(3.593811064887,-2.84776817148023,2.71146424332989));
#7204=CARTESIAN_POINT('Origin',(11.0238490761438,0.,0.));
#7205=CARTESIAN_POINT('Ctrl Pts',(3.89604095641107,-2.84679354424148,-2.71057216472783));
#7206=CARTESIAN_POINT('Ctrl Pts',(3.92579061605778,-2.44052785873738,-3.13624583529209));
#7207=CARTESIAN_POINT('Ctrl Pts',(4.00347068820956,-1.13491021990779,-4.01486290103005));
#7208=CARTESIAN_POINT('Ctrl Pts',(4.11090042000803,1.13491021990785,-4.01486290102993));
#7209=CARTESIAN_POINT('Ctrl Pts',(4.1885804921598,2.44052785873742,-3.13624583529207));
#7210=CARTESIAN_POINT('Ctrl Pts',(4.21833015180651,2.84679354424151,-2.71057216472779));
#7211=CARTESIAN_POINT('Origin',(11.0238490761438,0.,0.));
#7212=CARTESIAN_POINT('Ctrl Pts',(4.52104095641107,2.84678837447174,2.71057037657591));
#7213=CARTESIAN_POINT('Ctrl Pts',(4.55079061605777,2.44051811330425,3.13624232474605));
#7214=CARTESIAN_POINT('Ctrl Pts',(4.62847068820955,1.13488557063109,4.01485267650142));
#7215=CARTESIAN_POINT('Ctrl Pts',(4.73590042000803,-1.13488557063111,4.01485267650135));
#7216=CARTESIAN_POINT('Ctrl Pts',(4.8135804921598,-2.44051811330426,3.13624232474605));
#7217=CARTESIAN_POINT('Ctrl Pts',(4.84333015180651,-2.84678837447173,2.71057037657592));
#7218=CARTESIAN_POINT('Origin',(11.0238490761438,0.,0.));
#7219=CARTESIAN_POINT('Ctrl Pts',(5.14604095641107,-2.84678351585588,-2.71056863339249));
#7220=CARTESIAN_POINT('Ctrl Pts',(5.17579061605778,-2.44050895442134,-3.13623890248327));
#7221=CARTESIAN_POINT('Ctrl Pts',(5.25347068820956,-1.13486240492507,-4.01484270909931));
#7222=CARTESIAN_POINT('Ctrl Pts',(5.36090042000802,1.13486240492515,-4.01484270909921));
#7223=CARTESIAN_POINT('Ctrl Pts',(5.4385804921598,2.44050895442139,-3.13623890248322));
#7224=CARTESIAN_POINT('Ctrl Pts',(5.46833015180651,2.84678351585592,-2.71056863339245));
#7225=CARTESIAN_POINT('Origin',(11.0238490761438,0.,0.));
#7226=CARTESIAN_POINT('Ctrl Pts',(5.77104095641107,2.84677894112342,2.71056693350226));
#7227=CARTESIAN_POINT('Ctrl Pts',(5.80079061605777,2.44050033068152,3.13623556521482));
#7228=CARTESIAN_POINT('Ctrl Pts',(5.87847068820954,1.13484059276487,4.01483298924472));
#7229=CARTESIAN_POINT('Ctrl Pts',(5.98590042000804,-1.13484059276507,4.01483298924472));
#7230=CARTESIAN_POINT('Ctrl Pts',(6.0635804921598,-2.44050033068153,3.13623556521481));
#7231=CARTESIAN_POINT('Ctrl Pts',(6.0933301518065,-2.84677894112342,2.71056693350226));
#7232=CARTESIAN_POINT('Origin',(11.0238490761438,0.,0.));
#7233=CARTESIAN_POINT('Ctrl Pts',(6.39604095641106,-2.8467746261001,-2.7105652753122));
#7234=CARTESIAN_POINT('Ctrl Pts',(6.42579061605777,-2.44049219651438,-3.13623230981321));
#7235=CARTESIAN_POINT('Ctrl Pts',(6.50347068820954,-1.13482001888854,-4.01482350782885));
#7236=CARTESIAN_POINT('Ctrl Pts',(6.61090042000804,1.13482001888872,-4.01482350782888));
#7237=CARTESIAN_POINT('Ctrl Pts',(6.6885804921598,2.44049219651441,-3.13623230981319));
#7238=CARTESIAN_POINT('Ctrl Pts',(6.71833015180651,2.84677462610012,-2.71056527531218));
#7239=CARTESIAN_POINT('Origin',(11.0238490761438,0.,0.));
#7240=CARTESIAN_POINT('Ctrl Pts',(7.02104095641106,2.84677054928067,2.71056365730649));
#7241=CARTESIAN_POINT('Ctrl Pts',(7.05079061605777,2.4404845113808,3.13622913330255));
#7242=CARTESIAN_POINT('Ctrl Pts',(7.12847068820954,1.13480058075977,4.01481425618423));
#7243=CARTESIAN_POINT('Ctrl Pts',(7.23590042000803,-1.13480058075978,4.01481425618427));
#7244=CARTESIAN_POINT('Ctrl Pts',(7.3135804921598,-2.4404845113808,3.13622913330254));
#7245=CARTESIAN_POINT('Ctrl Pts',(7.34333015180651,-2.84677054928066,2.7105636573065));
#7246=CARTESIAN_POINT('Origin',(11.0238490761438,0.,0.));
#7247=CARTESIAN_POINT('Ctrl Pts',(7.64604095641107,-2.84676669147043,-2.71056207804189));
#7248=CARTESIAN_POINT('Ctrl Pts',(7.67579061605778,-2.44047723909725,-3.1362260328494));
#7249=CARTESIAN_POINT('Ctrl Pts',(7.75347068820955,-1.13478218685908,-4.01480522605852));
#7250=CARTESIAN_POINT('Ctrl Pts',(7.86090042000803,1.13478218685912,-4.01480522605852));
#7251=CARTESIAN_POINT('Ctrl Pts',(7.9385804921598,2.4404772390973,-3.13622603284936));
#7252=CARTESIAN_POINT('Ctrl Pts',(7.96833015180651,2.84676669147048,-2.71056207804184));
#7253=CARTESIAN_POINT('Origin',(11.0238490761438,0.,0.));
#7254=CARTESIAN_POINT('Ctrl Pts',(8.27104095641106,2.84676303548313,2.71056053614337));
#7255=CARTESIAN_POINT('Ctrl Pts',(8.30079061605777,2.44047034726616,3.1362230057544));
#7256=CARTESIAN_POINT('Ctrl Pts',(8.37847068820953,1.13476475524287,4.01479640958965));
#7257=CARTESIAN_POINT('Ctrl Pts',(8.48590042000803,-1.13476475524271,4.01479640958985));
#7258=CARTESIAN_POINT('Ctrl Pts',(8.56358049215979,-2.44047034726616,3.1362230057544));
#7259=CARTESIAN_POINT('Ctrl Pts',(8.59333015180651,-2.84676303548312,2.71056053614338));
#7260=CARTESIAN_POINT('Origin',(11.0238490761438,0.,0.));
#7261=CARTESIAN_POINT('Ctrl Pts',(8.89604095641106,-2.84675956588473,-2.71055903030038));
#7262=CARTESIAN_POINT('Ctrl Pts',(8.92579061605777,-2.44046380679322,-3.1362200494445));
#7263=CARTESIAN_POINT('Ctrl Pts',(9.00347068820953,-1.13474821232218,-4.01478779928378));
#7264=CARTESIAN_POINT('Ctrl Pts',(9.11090042000803,1.13474821232205,-4.01478779928393));
#7265=CARTESIAN_POINT('Ctrl Pts',(9.18858049215979,2.44046380679323,-3.1362200494445));
#7266=CARTESIAN_POINT('Ctrl Pts',(9.21833015180651,2.84675956588473,-2.71055903030039));
#7267=CARTESIAN_POINT('Origin',(11.0238490761438,0.,0.));
#7268=CARTESIAN_POINT('Ctrl Pts',(9.52104095641107,2.84675626877589,2.71055755926284));
#7269=CARTESIAN_POINT('Ctrl Pts',(9.55079061605777,2.44045759147703,3.13621716146554));
#7270=CARTESIAN_POINT('Ctrl Pts',(9.62847068820954,1.1347324918254,4.01477938799309));
#7271=CARTESIAN_POINT('Ctrl Pts',(9.73590042000802,-1.13473249182541,4.01477938799308));
#7272=CARTESIAN_POINT('Ctrl Pts',(9.81358049215979,-2.44045759147703,3.13621716146554));
#7273=CARTESIAN_POINT('Ctrl Pts',(9.84333015180651,-2.84675626877588,2.71055755926285));
#7274=CARTESIAN_POINT('Origin',(11.0238490761438,0.,0.));
#7275=CARTESIAN_POINT('Ctrl Pts',(10.1460409564111,-2.84675313160574,-2.7105561218378));
#7276=CARTESIAN_POINT('Ctrl Pts',(10.1757906160578,-2.44045167765816,-3.13621433947552));
#7277=CARTESIAN_POINT('Ctrl Pts',(10.2534706882095,-1.13471753391067,-4.01477116889627));
#7278=CARTESIAN_POINT('Ctrl Pts',(10.360900420008,1.13471753391068,-4.01477116889624));
#7279=CARTESIAN_POINT('Ctrl Pts',(10.4385804921598,2.44045167765817,-3.13621433947552));
#7280=CARTESIAN_POINT('Ctrl Pts',(10.4683301518065,2.84675313160573,-2.71055612183781));
#7281=CARTESIAN_POINT('Ctrl Pts',(4.27290740952806,3.47674578943201,-1.83867552770464));
#7282=CARTESIAN_POINT('Ctrl Pts',(4.22496533064083,3.03366144096162,-2.67651685389203));
#7283=CARTESIAN_POINT('Ctrl Pts',(4.12909283924855,1.51928728527458,-4.01486290102995));
#7284=CARTESIAN_POINT('Ctrl Pts',(3.98527826896903,-1.51928728527452,-4.01486290102998));
#7285=CARTESIAN_POINT('Ctrl Pts',(3.88940577757674,-3.03366144096159,-2.67651685389207));
#7286=CARTESIAN_POINT('Ctrl Pts',(3.84146369868952,-3.47674578943198,-1.8386755277047));
#7287=CARTESIAN_POINT('Ctrl Pts',(4.13588920451707,3.26695428751823,-1.72772738140596));
#7288=CARTESIAN_POINT('Ctrl Pts',(4.08794712562984,2.85060624264031,-2.51501223874808));
#7289=CARTESIAN_POINT('Ctrl Pts',(3.99207463423756,1.42761145370095,-3.7726006911942));
#7290=CARTESIAN_POINT('Ctrl Pts',(3.84826006395804,-1.42761145370091,-3.77260069119421));
#7291=CARTESIAN_POINT('Ctrl Pts',(3.75238757256575,-2.85060624264028,-2.51501223874812));
#7292=CARTESIAN_POINT('Ctrl Pts',(3.70444549367851,-3.26695428751821,-1.72772738140599));
#7293=CARTESIAN_POINT('Ctrl Pts',(3.99887099950606,3.05716278560445,-1.61677923510726));
#7294=CARTESIAN_POINT('Ctrl Pts',(3.95092892061883,2.667551044319,-2.35350762360415));
#7295=CARTESIAN_POINT('Ctrl Pts',(3.85505642922655,1.33593562212733,-3.53033848135843));
#7296=CARTESIAN_POINT('Ctrl Pts',(3.71124185894703,-1.3359356221273,-3.53033848135844));
#7297=CARTESIAN_POINT('Ctrl Pts',(3.61536936755474,-2.66755104431898,-2.35350762360417));
#7298=CARTESIAN_POINT('Ctrl Pts',(3.56742728866751,-3.05716278560443,-1.61677923510729));
#7299=CARTESIAN_POINT('Ctrl Pts',(3.86185279449507,2.84737128369067,-1.50583108880857));
#7300=CARTESIAN_POINT('Ctrl Pts',(3.81391071560784,2.48449584599769,-2.19200300846021));
#7301=CARTESIAN_POINT('Ctrl Pts',(3.71803822421555,1.2442597905537,-3.28807627152267));
#7302=CARTESIAN_POINT('Ctrl Pts',(3.57422365393604,-1.24425979055368,-3.28807627152268));
#7303=CARTESIAN_POINT('Ctrl Pts',(3.47835116254375,-2.48449584599768,-2.19200300846022));
#7304=CARTESIAN_POINT('Ctrl Pts',(3.43040908365653,-2.84737128369066,-1.50583108880859));
#7305=CARTESIAN_POINT('Ctrl Pts',(5.52290755913492,3.47674717210332,-1.83867291315533));
#7306=CARTESIAN_POINT('Ctrl Pts',(5.47496543037874,3.03366303203899,-2.67651546652179));
#7307=CARTESIAN_POINT('Ctrl Pts',(5.3790928891175,1.51922432968233,-4.01484270909923));
#7308=CARTESIAN_POINT('Ctrl Pts',(5.23527821910008,-1.51922432968225,-4.01484270909927));
#7309=CARTESIAN_POINT('Ctrl Pts',(5.13940567783883,-3.03366303203894,-2.67651546652185));
#7310=CARTESIAN_POINT('Ctrl Pts',(5.09146354908265,-3.47674717210328,-1.83867291315541));
#7311=CARTESIAN_POINT('Ctrl Pts',(5.38589301138905,3.26696118647632,-1.72772788602568));
#7312=CARTESIAN_POINT('Ctrl Pts',(5.33795088263287,2.85061262378872,-2.51501524594334));
#7313=CARTESIAN_POINT('Ctrl Pts',(5.24207834137162,1.42755474382685,-3.77258818405817));
#7314=CARTESIAN_POINT('Ctrl Pts',(5.0982636713542,-1.42755474382678,-3.7725881840582));
#7315=CARTESIAN_POINT('Ctrl Pts',(5.00239113009296,-2.85061262378867,-2.5150152459434));
#7316=CARTESIAN_POINT('Ctrl Pts',(4.95444900133677,-3.26696118647629,-1.72772788602574));
#7317=CARTESIAN_POINT('Ctrl Pts',(5.24887846364316,3.05717520084931,-1.61678285889602));
#7318=CARTESIAN_POINT('Ctrl Pts',(5.20093633488698,2.66756221553844,-2.3535150253649));
#7319=CARTESIAN_POINT('Ctrl Pts',(5.10506379362574,1.33588515797135,-3.5303336590171));
#7320=CARTESIAN_POINT('Ctrl Pts',(4.96124912360832,-1.3358851579713,-3.53033365901712));
#7321=CARTESIAN_POINT('Ctrl Pts',(4.86537658234707,-2.6675622155384,-2.35351502536494));
#7322=CARTESIAN_POINT('Ctrl Pts',(4.81743445359089,-3.05717520084929,-1.61678285889607));
#7323=CARTESIAN_POINT('Ctrl Pts',(5.11186391589729,2.84738921522231,-1.50583783176637));
#7324=CARTESIAN_POINT('Ctrl Pts',(5.06392178714111,2.48451180728816,-2.19201480478645));
#7325=CARTESIAN_POINT('Ctrl Pts',(4.96804924587987,1.24421557211587,-3.28807913397604));
#7326=CARTESIAN_POINT('Ctrl Pts',(4.82423457586244,-1.24421557211583,-3.28807913397605));
#7327=CARTESIAN_POINT('Ctrl Pts',(4.7283620346012,-2.48451180728813,-2.19201480478648));
#7328=CARTESIAN_POINT('Ctrl Pts',(4.68041990584502,-2.84738921522229,-1.50583783176641));
#7329=CARTESIAN_POINT('Ctrl Pts',(6.77290769409362,3.47674841939408,-1.83867055459827));
#7330=CARTESIAN_POINT('Ctrl Pts',(6.72496552035121,3.03366446720085,-2.67651421526794));
#7331=CARTESIAN_POINT('Ctrl Pts',(6.62909293410373,1.51916853850403,-4.01482350782886));
#7332=CARTESIAN_POINT('Ctrl Pts',(6.48527817411384,-1.51916853850395,-4.01482350782889));
#7333=CARTESIAN_POINT('Ctrl Pts',(6.38940558786636,-3.0336644672008,-2.676514215268));
#7334=CARTESIAN_POINT('Ctrl Pts',(6.34146341412395,-3.47674841939404,-1.83867055459834));
#7335=CARTESIAN_POINT('Ctrl Pts',(6.63589656027986,3.26696758565425,-1.72772843414892));
#7336=CARTESIAN_POINT('Ctrl Pts',(6.58795438653744,2.85061853334314,-2.51501809421893));
#7337=CARTESIAN_POINT('Ctrl Pts',(6.49208180028997,1.42750460308064,-3.7725761775094));
#7338=CARTESIAN_POINT('Ctrl Pts',(6.34826704030007,-1.42750460308057,-3.77257617750942));
#7339=CARTESIAN_POINT('Ctrl Pts',(6.25239445405259,-2.85061853334309,-2.51501809421899));
#7340=CARTESIAN_POINT('Ctrl Pts',(6.20445228031018,-3.26696758565422,-1.72772843414898));
#7341=CARTESIAN_POINT('Ctrl Pts',(6.49888542646609,3.05718675191442,-1.61678631369958));
#7342=CARTESIAN_POINT('Ctrl Pts',(6.45094325272367,2.66757259948543,-2.35352197316993));
#7343=CARTESIAN_POINT('Ctrl Pts',(6.35507066647619,1.33584066765725,-3.53032884718994));
#7344=CARTESIAN_POINT('Ctrl Pts',(6.2112559064863,-1.3358406676572,-3.53032884718996));
#7345=CARTESIAN_POINT('Ctrl Pts',(6.11538332023882,-2.66757259948539,-2.35352197316997));
#7346=CARTESIAN_POINT('Ctrl Pts',(6.0674411464964,-3.0571867519144,-1.61678631369962));
#7347=CARTESIAN_POINT('Ctrl Pts',(6.36187429265231,2.84740591817458,-1.50584419325024));
#7348=CARTESIAN_POINT('Ctrl Pts',(6.3139321189099,2.48452666562772,-2.19202585212091));
#7349=CARTESIAN_POINT('Ctrl Pts',(6.21805953266242,1.24417673223386,-3.28808151687049));
#7350=CARTESIAN_POINT('Ctrl Pts',(6.07424477267253,-1.24417673223382,-3.28808151687051));
#7351=CARTESIAN_POINT('Ctrl Pts',(5.97837218642505,-2.4845266656277,-2.19202585212095));
#7352=CARTESIAN_POINT('Ctrl Pts',(5.93043001268264,-2.84740591817456,-1.50584419325028));
#7353=CARTESIAN_POINT('Ctrl Pts',(8.02290781660591,3.47674955165342,-1.83866841355563));
#7354=CARTESIAN_POINT('Ctrl Pts',(7.97496560202607,3.03366576988594,-2.67651307964991));
#7355=CARTESIAN_POINT('Ctrl Pts',(7.87909297494116,1.51911875599997,-4.01480522605851));
#7356=CARTESIAN_POINT('Ctrl Pts',(7.73527813327642,-1.51911875599992,-4.01480522605853));
#7357=CARTESIAN_POINT('Ctrl Pts',(7.6394055061915,-3.03366576988591,-2.67651307964995));
#7358=CARTESIAN_POINT('Ctrl Pts',(7.59146329161166,-3.4767495516534,-1.83866841355567));
#7359=CARTESIAN_POINT('Ctrl Pts',(7.88589988091443,3.26697354631375,-1.72772901190777));
#7360=CARTESIAN_POINT('Ctrl Pts',(7.83795766633459,2.85062403009778,-2.51502079677286));
#7361=CARTESIAN_POINT('Ctrl Pts',(7.74208503924968,1.42745996391967,-3.77256465335495));
#7362=CARTESIAN_POINT('Ctrl Pts',(7.59827019758493,-1.42745996391964,-3.77256465335497));
#7363=CARTESIAN_POINT('Ctrl Pts',(7.50239757050003,-2.85062403009776,-2.51502079677288));
#7364=CARTESIAN_POINT('Ctrl Pts',(7.45445535592019,-3.26697354631373,-1.7277290119078));
#7365=CARTESIAN_POINT('Ctrl Pts',(7.74889194522295,3.05719754097409,-1.61678961025991));
#7366=CARTESIAN_POINT('Ctrl Pts',(7.7009497306431,2.66758229030962,-2.35352851389579));
#7367=CARTESIAN_POINT('Ctrl Pts',(7.6050771035582,1.33580117183938,-3.5303240806514));
#7368=CARTESIAN_POINT('Ctrl Pts',(7.46126226189346,-1.33580117183935,-3.53032408065141));
#7369=CARTESIAN_POINT('Ctrl Pts',(7.36538963480854,-2.6675822903096,-2.35352851389581));
#7370=CARTESIAN_POINT('Ctrl Pts',(7.3174474202287,-3.05719754097408,-1.61678961025993));
#7371=CARTESIAN_POINT('Ctrl Pts',(7.61188400953148,2.84742153563442,-1.50585020861204));
#7372=CARTESIAN_POINT('Ctrl Pts',(7.56394179495163,2.48454055052145,-2.19203623101873));
#7373=CARTESIAN_POINT('Ctrl Pts',(7.46806916786671,1.24414237975909,-3.28808350794784));
#7374=CARTESIAN_POINT('Ctrl Pts',(7.32425432620197,-1.24414237975908,-3.28808350794785));
#7375=CARTESIAN_POINT('Ctrl Pts',(7.22838169911706,-2.48454055052144,-2.19203623101874));
#7376=CARTESIAN_POINT('Ctrl Pts',(7.18043948453722,-2.84742153563441,-1.50585020861206));
#7377=CARTESIAN_POINT('Ctrl Pts',(9.27290792843865,3.47675058521116,-1.83866645914951));
#7378=CARTESIAN_POINT('Ctrl Pts',(9.22496567658123,3.03366695890456,-2.67651204323431));
#7379=CARTESIAN_POINT('Ctrl Pts',(9.12909301221873,1.51907406221497,-4.01478779928389));
#7380=CARTESIAN_POINT('Ctrl Pts',(8.98527809599884,-1.51907406221493,-4.0147877992839));
#7381=CARTESIAN_POINT('Ctrl Pts',(8.88940543163634,-3.03366695890454,-2.67651204323434));
#7382=CARTESIAN_POINT('Ctrl Pts',(8.84146317977892,-3.47675058521115,-1.83866645914954));
#7383=CARTESIAN_POINT('Ctrl Pts',(9.13590299800969,3.26697911893791,-1.72772960887218));
#7384=CARTESIAN_POINT('Ctrl Pts',(9.08796074615226,2.85062916238817,-2.51502336521541));
#7385=CARTESIAN_POINT('Ctrl Pts',(8.99208808178978,1.42741997728753,-3.77255359156877));
#7386=CARTESIAN_POINT('Ctrl Pts',(8.84827316556986,-1.4274199772875,-3.77255359156878));
#7387=CARTESIAN_POINT('Ctrl Pts',(8.75240050120738,-2.85062916238816,-2.51502336521541));
#7388=CARTESIAN_POINT('Ctrl Pts',(8.70445824934996,-3.2669791189379,-1.72772960887219));
#7389=CARTESIAN_POINT('Ctrl Pts',(8.99889806758071,3.05720765266466,-1.61679275859484));
#7390=CARTESIAN_POINT('Ctrl Pts',(8.95095581572329,2.66759136587177,-2.35353468719648));
#7391=CARTESIAN_POINT('Ctrl Pts',(8.85508315136081,1.33576589236007,-3.53031938385365));
#7392=CARTESIAN_POINT('Ctrl Pts',(8.71126823514089,-1.33576589236006,-3.53031938385365));
#7393=CARTESIAN_POINT('Ctrl Pts',(8.61539557077841,-2.66759136587176,-2.35353468719649));
#7394=CARTESIAN_POINT('Ctrl Pts',(8.56745331892098,-3.05720765266466,-1.61679275859485));
#7395=CARTESIAN_POINT('Ctrl Pts',(8.86189313715175,2.84743618639142,-1.5058559083175));
#7396=CARTESIAN_POINT('Ctrl Pts',(8.81395088529433,2.48455356935539,-2.19204600917757));
#7397=CARTESIAN_POINT('Ctrl Pts',(8.71807822093185,1.24411180743262,-3.28808517613852));
#7398=CARTESIAN_POINT('Ctrl Pts',(8.57426330471193,-1.24411180743262,-3.28808517613852));
#7399=CARTESIAN_POINT('Ctrl Pts',(8.47839064034944,-2.48455356935539,-2.19204600917757));
#7400=CARTESIAN_POINT('Ctrl Pts',(8.43044838849202,-2.84743618639142,-1.5058559083175));
#7401=CARTESIAN_POINT('Ctrl Pts',(10.5229080310278,3.47675153333854,-1.83866466628547));
#7402=CARTESIAN_POINT('Ctrl Pts',(10.474965744974,3.03366804954435,-2.67651109266735));
#7403=CARTESIAN_POINT('Ctrl Pts',(10.3790930464151,1.51903371577996,-4.01477116889625));
#7404=CARTESIAN_POINT('Ctrl Pts',(10.2352780618025,-1.51903371577993,-4.01477116889626));
#7405=CARTESIAN_POINT('Ctrl Pts',(10.1394053632436,-3.03366804954433,-2.67651109266738));
#7406=CARTESIAN_POINT('Ctrl Pts',(10.0914630771898,-3.47675153333853,-1.8386646662855));
#7407=CARTESIAN_POINT('Ctrl Pts',(10.3859059323742,3.26698434565854,-1.72773021714958));
#7408=CARTESIAN_POINT('Ctrl Pts',(10.3379636463205,2.85063397046062,-2.51502580983381));
#7409=CARTESIAN_POINT('Ctrl Pts',(10.2420909477615,1.4273839595363,-3.77254297133811));
#7410=CARTESIAN_POINT('Ctrl Pts',(10.0982759631489,-1.42738395953627,-3.77254297133812));
#7411=CARTESIAN_POINT('Ctrl Pts',(10.00240326459,-2.85063397046061,-2.51502580983382));
#7412=CARTESIAN_POINT('Ctrl Pts',(9.95446097853621,-3.26698434565853,-1.7277302171496));
#7413=CARTESIAN_POINT('Ctrl Pts',(10.2489038337206,3.05721715797854,-1.61679576801369));
#7414=CARTESIAN_POINT('Ctrl Pts',(10.2009615476668,2.66759989137687,-2.35354052700025));
#7415=CARTESIAN_POINT('Ctrl Pts',(10.105088849108,1.33573420329263,-3.53031477377997));
#7416=CARTESIAN_POINT('Ctrl Pts',(9.96127386449531,-1.33573420329262,-3.53031477377997));
#7417=CARTESIAN_POINT('Ctrl Pts',(9.86540116593643,-2.66759989137686,-2.35354052700027));
#7418=CARTESIAN_POINT('Ctrl Pts',(9.81745887988263,-3.05721715797854,-1.6167957680137));
#7419=CARTESIAN_POINT('Ctrl Pts',(10.111901735067,2.84744997029854,-1.5058613188778));
#7420=CARTESIAN_POINT('Ctrl Pts',(10.0639594490133,2.48456581229314,-2.19205524416672));
#7421=CARTESIAN_POINT('Ctrl Pts',(9.96808675045439,1.24408444704895,-3.28808657622182));
#7422=CARTESIAN_POINT('Ctrl Pts',(9.82427176584173,-1.24408444704895,-3.28808657622182));
#7423=CARTESIAN_POINT('Ctrl Pts',(9.72839906728286,-2.48456581229314,-2.19205524416672));
#7424=CARTESIAN_POINT('Ctrl Pts',(9.68045678122906,-2.84744997029854,-1.5058613188778));
#7425=CARTESIAN_POINT('Ctrl Pts',(3.64838128925859,-3.47740286631016,1.83922164452567));
#7426=CARTESIAN_POINT('Ctrl Pts',(3.60379518879799,-3.06521053407891,2.61855938315106));
#7427=CARTESIAN_POINT('Ctrl Pts',(3.51463169441755,-1.69992623500153,3.88752819359771));
#7428=CARTESIAN_POINT('Ctrl Pts',(3.38089080611729,1.09279645395022,4.09974510230776));
#7429=CARTESIAN_POINT('Ctrl Pts',(3.29173601827763,2.63403351313429,3.0518682259016));
#7430=CARTESIAN_POINT('Ctrl Pts',(3.24715862435781,3.1592487603224,2.34397402547678));
#7431=CARTESIAN_POINT('Ctrl Pts',(3.51131387403993,-3.26754097150884,1.72822428410498));
#7432=CARTESIAN_POINT('Ctrl Pts',(3.46672777357933,-2.88022452142018,2.46052884860418));
#7433=CARTESIAN_POINT('Ctrl Pts',(3.37756427919888,-1.59733537785462,3.65291516077772));
#7434=CARTESIAN_POINT('Ctrl Pts',(3.24382339089863,1.02684598940094,3.85232474048881));
#7435=CARTESIAN_POINT('Ctrl Pts',(3.15466860305897,2.47506911203139,2.86768742396558));
#7436=CARTESIAN_POINT('Ctrl Pts',(3.11009120913914,2.9685875236238,2.20251476715576));
#7437=CARTESIAN_POINT('Ctrl Pts',(3.37424645882128,-3.05767907670752,1.61722692368431));
#7438=CARTESIAN_POINT('Ctrl Pts',(3.32966035836067,-2.69523850876146,2.30249831405731));
#7439=CARTESIAN_POINT('Ctrl Pts',(3.24049686398023,-1.4947445207077,3.41830212795774));
#7440=CARTESIAN_POINT('Ctrl Pts',(3.10675597567997,0.960895524851675,3.60490437866986));
#7441=CARTESIAN_POINT('Ctrl Pts',(3.01760118784032,2.31610471092849,2.68350662202955));
#7442=CARTESIAN_POINT('Ctrl Pts',(2.97302379392049,2.77792628692519,2.06105550883474));
#7443=CARTESIAN_POINT('Ctrl Pts',(3.23717904360261,-2.84781718190621,1.50622956326363));
#7444=CARTESIAN_POINT('Ctrl Pts',(3.192592943142,-2.51025249610272,2.14446777951043));
#7445=CARTESIAN_POINT('Ctrl Pts',(3.10342944876156,-1.39215366356079,3.18368909513775));
#7446=CARTESIAN_POINT('Ctrl Pts',(2.96968856046131,0.8949450603024,3.35748401685091));
#7447=CARTESIAN_POINT('Ctrl Pts',(2.88053377262165,2.15714030982559,2.49932582009352));
#7448=CARTESIAN_POINT('Ctrl Pts',(2.83595637870183,2.5872650502266,1.91959625051372));
#7449=CARTESIAN_POINT('Ctrl Pts',(4.89790748632074,-3.47674649915261,1.83867418566579));
#7450=CARTESIAN_POINT('Ctrl Pts',(4.84996538183595,-3.03366225767408,2.67651614172047));
#7451=CARTESIAN_POINT('Ctrl Pts',(4.7540928648461,-1.51925482848182,4.01485267650136));
#7452=CARTESIAN_POINT('Ctrl Pts',(4.61027824337146,1.51925482848179,4.01485267650137));
#7453=CARTESIAN_POINT('Ctrl Pts',(4.51440572638162,3.03366225767406,2.67651614172049));
#7454=CARTESIAN_POINT('Ctrl Pts',(4.46646362189683,3.47674649915259,1.83867418566581));
#7455=CARTESIAN_POINT('Ctrl Pts',(4.76089114229214,-3.26695780380383,1.72772762724506));
#7456=CARTESIAN_POINT('Ctrl Pts',(4.71294903780735,-2.85060949632914,2.51501376310635));
#7457=CARTESIAN_POINT('Ctrl Pts',(4.6170765208175,-1.42758220050988,3.77259437402633));
#7458=CARTESIAN_POINT('Ctrl Pts',(4.47326189934286,1.42758220050987,3.77259437402634));
#7459=CARTESIAN_POINT('Ctrl Pts',(4.37738938235302,2.85060949632913,2.51501376310635));
#7460=CARTESIAN_POINT('Ctrl Pts',(4.32944727786822,3.26695780380383,1.72772762724508));
#7461=CARTESIAN_POINT('Ctrl Pts',(4.62387479826355,-3.05716910845506,1.61678106882435));
#7462=CARTESIAN_POINT('Ctrl Pts',(4.57593269377875,-2.66755673498418,2.35351138449224));
#7463=CARTESIAN_POINT('Ctrl Pts',(4.48006017678891,-1.33590957253795,3.5303360715513));
#7464=CARTESIAN_POINT('Ctrl Pts',(4.33624555531426,1.33590957253794,3.5303360715513));
#7465=CARTESIAN_POINT('Ctrl Pts',(4.24037303832442,2.66755673498418,2.35351138449224));
#7466=CARTESIAN_POINT('Ctrl Pts',(4.19243093383963,3.05716910845506,1.61678106882436));
#7467=CARTESIAN_POINT('Ctrl Pts',(4.48685845423494,-2.8473804131063,1.50583451040362));
#7468=CARTESIAN_POINT('Ctrl Pts',(4.43891634975015,-2.48450397363924,2.19200900587812));
#7469=CARTESIAN_POINT('Ctrl Pts',(4.34304383276031,-1.24423694456603,3.28807776907627));
#7470=CARTESIAN_POINT('Ctrl Pts',(4.19922921128567,1.24423694456603,3.28807776907627));
#7471=CARTESIAN_POINT('Ctrl Pts',(4.10335669429582,2.48450397363925,2.19200900587812));
#7472=CARTESIAN_POINT('Ctrl Pts',(4.05541458981104,2.84738041310631,1.50583451040362));
#7473=CARTESIAN_POINT('Ctrl Pts',(6.14790762829603,-3.47674781129169,1.8386717044864));
#7474=CARTESIAN_POINT('Ctrl Pts',(6.09996547648614,-3.03366376752034,2.67651482526888));
#7475=CARTESIAN_POINT('Ctrl Pts',(6.0040929121712,-1.51919561710872,4.01483298924471));
#7476=CARTESIAN_POINT('Ctrl Pts',(5.86027819604637,1.51919561710867,4.01483298924473));
#7477=CARTESIAN_POINT('Ctrl Pts',(5.76440563173143,3.03366376752031,2.67651482526892));
#7478=CARTESIAN_POINT('Ctrl Pts',(5.71646347992155,3.47674781129167,1.83867170448645));
#7479=CARTESIAN_POINT('Ctrl Pts',(6.01089481609153,-3.26696444442227,1.72772815560951));
#7480=CARTESIAN_POINT('Ctrl Pts',(5.96295266428165,-2.85061563356214,2.51501668908045));
#7481=CARTESIAN_POINT('Ctrl Pts',(5.8670800999667,-1.42752892490422,3.77258211928897));
#7482=CARTESIAN_POINT('Ctrl Pts',(5.72326538384188,1.42752892490418,3.77258211928898));
#7483=CARTESIAN_POINT('Ctrl Pts',(5.62739281952693,2.85061563356211,2.51501668908049));
#7484=CARTESIAN_POINT('Ctrl Pts',(5.57945066771705,3.26696444442225,1.72772815560954));
#7485=CARTESIAN_POINT('Ctrl Pts',(5.87388200388703,-3.05718107755285,1.61678460673262));
#7486=CARTESIAN_POINT('Ctrl Pts',(5.82593985207715,-2.66756749960396,2.35351855289203));
#7487=CARTESIAN_POINT('Ctrl Pts',(5.73006728776221,-1.33586223269973,3.53033124933322));
#7488=CARTESIAN_POINT('Ctrl Pts',(5.58625257163737,1.3358622326997,3.53033124933323));
#7489=CARTESIAN_POINT('Ctrl Pts',(5.49038000732244,2.66756749960394,2.35351855289205));
#7490=CARTESIAN_POINT('Ctrl Pts',(5.44243785551255,3.05718107755284,1.61678460673264));
#7491=CARTESIAN_POINT('Ctrl Pts',(5.73686919168254,-2.84739771068344,1.50584105785573));
#7492=CARTESIAN_POINT('Ctrl Pts',(5.68892703987265,-2.48451936564576,2.19202041670361));
#7493=CARTESIAN_POINT('Ctrl Pts',(5.59305447555771,-1.24419554049523,3.28808037937748));
#7494=CARTESIAN_POINT('Ctrl Pts',(5.44923975943288,1.24419554049521,3.28808037937748));
#7495=CARTESIAN_POINT('Ctrl Pts',(5.35336719511794,2.48451936564575,2.19202041670362));
#7496=CARTESIAN_POINT('Ctrl Pts',(5.30542504330806,2.84739771068344,1.50584105785575));
#7497=CARTESIAN_POINT('Ctrl Pts',(7.39790775678633,-3.47674899880063,1.83866945897147));
#7498=CARTESIAN_POINT('Ctrl Pts',(7.34996556214635,-3.03366513383357,2.67651363411353));
#7499=CARTESIAN_POINT('Ctrl Pts',(7.2540929550013,-1.51914295842827,4.01481425618425));
#7500=CARTESIAN_POINT('Ctrl Pts',(7.11027815321627,1.51914295842826,4.01481425618426));
#7501=CARTESIAN_POINT('Ctrl Pts',(7.01440554607122,3.03366513383357,2.67651363411354));
#7502=CARTESIAN_POINT('Ctrl Pts',(6.96646335143124,3.47674899880063,1.83866945897148));
#7503=CARTESIAN_POINT('Ctrl Pts',(7.26089824748156,-3.26697061742319,1.72772872004433));
#7504=CARTESIAN_POINT('Ctrl Pts',(7.21295605284158,-2.85062133008578,2.5150194629517));
#7505=CARTESIAN_POINT('Ctrl Pts',(7.11708344569652,-1.42748165328085,3.772570356356));
#7506=CARTESIAN_POINT('Ctrl Pts',(6.9732686439115,1.42748165328084,3.77257035635601));
#7507=CARTESIAN_POINT('Ctrl Pts',(6.87739603676645,2.85062133008577,2.51501946295171));
#7508=CARTESIAN_POINT('Ctrl Pts',(6.82945384212647,3.26697061742319,1.72772872004433));
#7509=CARTESIAN_POINT('Ctrl Pts',(7.12388873817679,-3.05719223604573,1.61678798111718));
#7510=CARTESIAN_POINT('Ctrl Pts',(7.07594654353681,-2.66757752633796,2.35352529178989));
#7511=CARTESIAN_POINT('Ctrl Pts',(6.98007393639176,-1.33582034813344,3.53032645652775));
#7512=CARTESIAN_POINT('Ctrl Pts',(6.83625913460674,1.33582034813344,3.53032645652775));
#7513=CARTESIAN_POINT('Ctrl Pts',(6.74038652746168,2.66757752633797,2.35352529178988));
#7514=CARTESIAN_POINT('Ctrl Pts',(6.6924443328217,3.05719223604573,1.61678798111717));
#7515=CARTESIAN_POINT('Ctrl Pts',(6.98687922887202,-2.84741385466828,1.50584724219002));
#7516=CARTESIAN_POINT('Ctrl Pts',(6.93893703423204,-2.48453372259017,2.19203112062806));
#7517=CARTESIAN_POINT('Ctrl Pts',(6.84306442708698,-1.24415904298601,3.28808255669949));
#7518=CARTESIAN_POINT('Ctrl Pts',(6.69924962530196,1.24415904298602,3.28808255669949));
#7519=CARTESIAN_POINT('Ctrl Pts',(6.60337701815691,2.48453372259019,2.19203112062805));
#7520=CARTESIAN_POINT('Ctrl Pts',(6.55543482351693,2.84741385466829,1.50584724219001));
#7521=CARTESIAN_POINT('Ctrl Pts',(8.64790787376072,-3.47675007987806,1.83866741470954));
#7522=CARTESIAN_POINT('Ctrl Pts',(8.59996564012927,-3.03366637757612,2.67651254993933));
#7523=CARTESIAN_POINT('Ctrl Pts',(8.50409299399277,-1.51909582299121,4.01479640958979));
#7524=CARTESIAN_POINT('Ctrl Pts',(8.3602781142248,1.51909582299119,4.0147964095898));
#7525=CARTESIAN_POINT('Ctrl Pts',(8.2644054680883,3.03366637757611,2.67651254993935));
#7526=CARTESIAN_POINT('Ctrl Pts',(8.21646323445685,3.47675007987805,1.83866741470956));
#7527=CARTESIAN_POINT('Ctrl Pts',(8.51090146352299,-3.26697637832471,1.72772930853349));
#7528=CARTESIAN_POINT('Ctrl Pts',(8.46295922989154,-2.85062663911888,2.51502209708675));
#7529=CARTESIAN_POINT('Ctrl Pts',(8.36708658375503,-1.42743943513422,3.77255906595759));
#7530=CARTESIAN_POINT('Ctrl Pts',(8.22327170398708,1.42743943513421,3.77255906595759));
#7531=CARTESIAN_POINT('Ctrl Pts',(8.12739905785057,2.85062663911887,2.51502209708676));
#7532=CARTESIAN_POINT('Ctrl Pts',(8.07945682421912,3.26697637832471,1.7277293085335));
#7533=CARTESIAN_POINT('Ctrl Pts',(8.37389505328524,-3.05720267677136,1.61679120235743));
#7534=CARTESIAN_POINT('Ctrl Pts',(8.32595281965381,-2.66758690066164,2.35353164423417));
#7535=CARTESIAN_POINT('Ctrl Pts',(8.23008017351729,-1.33578304727724,3.53032172232538));
#7536=CARTESIAN_POINT('Ctrl Pts',(8.08626529374934,1.33578304727724,3.53032172232538));
#7537=CARTESIAN_POINT('Ctrl Pts',(7.99039264761284,2.66758690066164,2.35353164423417));
#7538=CARTESIAN_POINT('Ctrl Pts',(7.94245041398138,3.05720267677136,1.61679120235743));
#7539=CARTESIAN_POINT('Ctrl Pts',(8.23688864304753,-2.84742897521801,1.50585309618137));
#7540=CARTESIAN_POINT('Ctrl Pts',(8.18894640941607,-2.48454716220439,2.1920411913816));
#7541=CARTESIAN_POINT('Ctrl Pts',(8.09307376327956,-1.24412665942025,3.28808437869317));
#7542=CARTESIAN_POINT('Ctrl Pts',(7.94925888351161,1.24412665942026,3.28808437869317));
#7543=CARTESIAN_POINT('Ctrl Pts',(7.85338623737511,2.4845471622044,2.19204119138159));
#7544=CARTESIAN_POINT('Ctrl Pts',(7.80544400374366,2.84742897521802,1.50585309618137));
#7545=CARTESIAN_POINT('Ctrl Pts',(9.89790798080964,-3.47675106922323,1.83866554390586));
#7546=CARTESIAN_POINT('Ctrl Pts',(9.84996571149522,-3.0336675156804,2.67651155795465));
#7547=CARTESIAN_POINT('Ctrl Pts',(9.75409302967573,-1.51905338615236,4.01477938799308));
#7548=CARTESIAN_POINT('Ctrl Pts',(9.61027807854184,1.51905338615236,4.01477938799308));
#7549=CARTESIAN_POINT('Ctrl Pts',(9.51440539672235,3.0336675156804,2.67651155795466));
#7550=CARTESIAN_POINT('Ctrl Pts',(9.46646312740793,3.47675106922323,1.83866554390586));
#7551=CARTESIAN_POINT('Ctrl Pts',(9.76090448686174,-3.26698177317707,1.72772991200983));
#7552=CARTESIAN_POINT('Ctrl Pts',(9.71296221754732,-2.85063160470143,2.51502460240538));
#7553=CARTESIAN_POINT('Ctrl Pts',(9.61708953572784,-1.42740150969491,3.77254822757006));
#7554=CARTESIAN_POINT('Ctrl Pts',(9.47327458459393,1.42740150969491,3.77254822757006));
#7555=CARTESIAN_POINT('Ctrl Pts',(9.37740190277446,2.85063160470144,2.51502460240537));
#7556=CARTESIAN_POINT('Ctrl Pts',(9.32945963346002,3.26698177317708,1.72772991200983));
#7557=CARTESIAN_POINT('Ctrl Pts',(9.62390099291383,-3.05721247713093,1.61679428011383));
#7558=CARTESIAN_POINT('Ctrl Pts',(9.57595872359942,-2.66759569372247,2.35353764685611));
#7559=CARTESIAN_POINT('Ctrl Pts',(9.48008604177992,-1.33574963323748,3.53031706714705));
#7560=CARTESIAN_POINT('Ctrl Pts',(9.33627109064602,1.33574963323749,3.53031706714703));
#7561=CARTESIAN_POINT('Ctrl Pts',(9.24039840882654,2.66759569372248,2.3535376468561));
#7562=CARTESIAN_POINT('Ctrl Pts',(9.19245613951212,3.05721247713093,1.61679428011382));
#7563=CARTESIAN_POINT('Ctrl Pts',(9.48689749896593,-2.84744318108477,1.5058586482178));
#7564=CARTESIAN_POINT('Ctrl Pts',(9.43895522965151,-2.4845597827435,2.19205069130684));
#7565=CARTESIAN_POINT('Ctrl Pts',(9.34308254783202,-1.24409775678003,3.28808590672403));
#7566=CARTESIAN_POINT('Ctrl Pts',(9.19926759669813,1.24409775678006,3.28808590672402));
#7567=CARTESIAN_POINT('Ctrl Pts',(9.10339491487864,2.48455978274351,2.19205069130682));
#7568=CARTESIAN_POINT('Ctrl Pts',(9.05545264556422,2.84744318108478,1.50585864821778));
#7569=CARTESIAN_POINT('Ctrl Pts',(11.1479080792332,-3.47675197885198,1.8386638238398));
#7570=CARTESIAN_POINT('Ctrl Pts',(11.0999657771109,-3.03366856198811,2.67651064606967));
#7571=CARTESIAN_POINT('Ctrl Pts',(11.0040930624836,-1.51901497956362,4.01476313548051));
#7572=CARTESIAN_POINT('Ctrl Pts',(10.860278045734,1.51901497956361,4.01476313548052));
#7573=CARTESIAN_POINT('Ctrl Pts',(10.7644053311067,3.0336685619881,2.67651064606967));
#7574=CARTESIAN_POINT('Ctrl Pts',(10.7164630289844,3.47675197885198,1.83866382383981));
#7575=CARTESIAN_POINT('Ctrl Pts',(11.01090733667,-3.26698684063499,1.72773052359626));
#7576=CARTESIAN_POINT('Ctrl Pts',(10.9629650345478,-2.85063626371641,2.51502698861378));
#7577=CARTESIAN_POINT('Ctrl Pts',(10.8670923199204,-1.42736726092277,3.77253782025955));
#7578=CARTESIAN_POINT('Ctrl Pts',(10.7232773031708,1.42736726092277,3.77253782025955));
#7579=CARTESIAN_POINT('Ctrl Pts',(10.6274045885434,2.85063626371641,2.51502698861378));
#7580=CARTESIAN_POINT('Ctrl Pts',(10.5794622864212,3.26698684063499,1.72773052359626));
#7581=CARTESIAN_POINT('Ctrl Pts',(10.8739065941069,-3.057221702418,1.61679722335272));
#7582=CARTESIAN_POINT('Ctrl Pts',(10.8259642919846,-2.6676039654447,2.35354333115788));
#7583=CARTESIAN_POINT('Ctrl Pts',(10.7300915773573,-1.33571954228192,3.53031250503859));
#7584=CARTESIAN_POINT('Ctrl Pts',(10.5862765606076,1.33571954228193,3.53031250503859));
#7585=CARTESIAN_POINT('Ctrl Pts',(10.4904038459803,2.66760396544471,2.35354333115788));
#7586=CARTESIAN_POINT('Ctrl Pts',(10.442461543858,3.05722170241801,1.61679722335272));
#7587=CARTESIAN_POINT('Ctrl Pts',(10.7369058515438,-2.84745656420101,1.50586392310919));
#7588=CARTESIAN_POINT('Ctrl Pts',(10.6889635494215,-2.484571667173,2.192059673702));
#7589=CARTESIAN_POINT('Ctrl Pts',(10.5930908347941,-1.24407182364107,3.28808718981763));
#7590=CARTESIAN_POINT('Ctrl Pts',(10.4492758180446,1.24407182364108,3.28808718981762));
#7591=CARTESIAN_POINT('Ctrl Pts',(10.3534031034172,2.48457166717301,2.19205967370197));
#7592=CARTESIAN_POINT('Ctrl Pts',(10.305460801295,2.84745656420102,1.50586392310916));
#7593=CARTESIAN_POINT('Origin',(11.0238490761438,-0.429849779945933,0.997913274973232));
#7594=CARTESIAN_POINT('Ctrl Pts',(11.1020448718976,-1.95024171098983,-2.73386013557053));
#7595=CARTESIAN_POINT('Ctrl Pts',(11.0712404028977,-2.37355302340116,-2.43188441726037));
#7596=CARTESIAN_POINT('Ctrl Pts',(11.0404359338978,-2.72516811805232,-2.03009223981615));
#7597=CARTESIAN_POINT('Ctrl Pts',(11.0096314648979,-2.96834053891712,-1.57047394666944));
#7598=CARTESIAN_POINT('Ctrl Pts',(11.0759796066463,-1.92402331790621,-2.69710704016389));
#7599=CARTESIAN_POINT('Ctrl Pts',(11.0451751376464,-2.34164377552606,-2.3991909817614));
#7600=CARTESIAN_POINT('Ctrl Pts',(11.0143706686465,-2.68853187520334,-2.00280036310181));
#7601=CARTESIAN_POINT('Ctrl Pts',(10.9835661996466,-2.9284351678973,-1.54936102357415));
#7602=CARTESIAN_POINT('Ctrl Pts',(11.049914341395,-1.8978049248226,-2.66035394475725));
#7603=CARTESIAN_POINT('Ctrl Pts',(11.0191098723951,-2.30973452765096,-2.36649754626242));
#7604=CARTESIAN_POINT('Ctrl Pts',(10.9883054033952,-2.65189563235436,-1.97550848638747));
#7605=CARTESIAN_POINT('Ctrl Pts',(10.9575009343953,-2.88852979687749,-1.52824810047886));
#7606=CARTESIAN_POINT('Ctrl Pts',(11.0238490761438,-1.87158653173898,-2.62360084935061));
#7607=CARTESIAN_POINT('Ctrl Pts',(10.9930446071439,-2.27782527977586,-2.33380411076345));
#7608=CARTESIAN_POINT('Ctrl Pts',(10.962240138144,-2.61525938950538,-1.94821660967313));
#7609=CARTESIAN_POINT('Ctrl Pts',(10.9314356691441,-2.84862442585768,-1.50713517738357));
#7610=CARTESIAN_POINT('Ctrl Pts',(11.0238490761438,-2.84858683313225,-1.77828791130292));
#7611=CARTESIAN_POINT('Ctrl Pts',(11.0238490761438,-2.71494761674313,-1.950099643838));
#7612=CARTESIAN_POINT('Ctrl Pts',(11.0238490760976,-2.56437727492177,-2.10888684210166));
#7613=CARTESIAN_POINT('Ctrl Pts',(11.0238490760976,-2.23653062661935,-2.39254456366359));
#7614=CARTESIAN_POINT('Ctrl Pts',(11.0238490761438,-2.05954305124027,-2.51769365192168));
#7615=CARTESIAN_POINT('Ctrl Pts',(11.0238490761438,-1.87158653173898,-2.62360084935061));
#7616=CARTESIAN_POINT('Origin',(11.0238490761438,0.,0.));
#7617=CARTESIAN_POINT('',(12.0768490761438,5.,-6.12323399573677E-16));
#7618=CARTESIAN_POINT('Origin',(12.0768490761438,0.,0.));
#7619=CARTESIAN_POINT('',(11.0238490761438,5.,-6.12323399573677E-16));
#7620=CARTESIAN_POINT('',(11.0238490761438,5.,6.12323399573677E-16));
#7621=CARTESIAN_POINT('Origin',(11.0238490761438,0.,0.));
#7622=CARTESIAN_POINT('Origin',(11.0238490761438,0.,0.));
#7623=CARTESIAN_POINT('Origin',(12.0768490761438,0.,0.));
#27688=UNCERTAINTY_MEASURE_WITH_UNIT(LENGTH_MEASURE(0.01),#27708,
'DISTANCE_ACCURACY_VALUE',
'Maximum model space distance between geometric entities at asserted c
onnectivities');
#27695=UNCERTAINTY_MEASURE_WITH_UNIT(LENGTH_MEASURE(0.01),#27708,
'DISTANCE_ACCURACY_VALUE',
'Maximum model space distance between geometric entities at asserted c
onnectivities');
#27700=(
GEOMETRIC_REPRESENTATION_CONTEXT(3)
GLOBAL_UNCERTAINTY_ASSIGNED_CONTEXT((#27688))
GLOBAL_UNIT_ASSIGNED_CONTEXT((#27708,#27710,#27711))
REPRESENTATION_CONTEXT('','3D')
);
#27707=(
GEOMETRIC_REPRESENTATION_CONTEXT(3)
GLOBAL_UNCERTAINTY_ASSIGNED_CONTEXT((#27695))
GLOBAL_UNIT_ASSIGNED_CONTEXT((#27708,#27710,#27711))
REPRESENTATION_CONTEXT('','3D')
);
#27708=(
LENGTH_UNIT()
NAMED_UNIT(*)
SI_UNIT(.MILLI.,.METRE.)
);
#27710=(
NAMED_UNIT(*)
PLANE_ANGLE_UNIT()
SI_UNIT($,.RADIAN.)
);
#27711=(
NAMED_UNIT(*)
SI_UNIT($,.STERADIAN.)
SOLID_ANGLE_UNIT()
);
#27716=SHAPE_DEFINITION_REPRESENTATION(#27727,#27748);
#27727=PRODUCT_DEFINITION_SHAPE('',$,#27760);
#27748=SHAPE_REPRESENTATION('',(#4008),#27700);
#27755=PRODUCT_DEFINITION_CONTEXT('part definition',#27790,'design');
#27760=PRODUCT_DEFINITION('Screw_02','Screw_02',#27771,#27755);
#27771=PRODUCT_DEFINITION_FORMATION('',$,#27796);
#27790=APPLICATION_CONTEXT(
'Core Data for Automotive Mechanical Design Process');
#27791=PRODUCT_CONTEXT('part definition',#27790,'mechanical');
#27796=PRODUCT('Screw_02','Screw_02',$,(#27791));
#27804=PRESENTATION_STYLE_ASSIGNMENT((#27806));
#27806=SURFACE_STYLE_USAGE(.BOTH.,#27808);
#27808=SURFACE_SIDE_STYLE('',(#27810));
#27810=SURFACE_STYLE_FILL_AREA(#27812);
#27812=FILL_AREA_STYLE('Opaque(160,160,160)',(#27814));
#27814=FILL_AREA_STYLE_COLOUR('Opaque(160,160,160)',#27816);
#27816=COLOUR_RGB('Opaque(160,160,160)', 0.09019608, 0.27058824, 0.51372549);
ENDSEC;
END-ISO-10303-21;
